ISO-10303-21;
HEADER;
/* Generated by software containing ST-Developer
 * from STEP Tools, Inc. (www.steptools.com) 
 */

FILE_DESCRIPTION(
/* description */ ('CAx-IF Rec.Pracs.---Representation and Presentation of Product Manufa
cturing Information (PMI)---4.0---2014-10-13'),
/* implementation_level */ '2;1');

FILE_NAME(
/* name */ 'Pan Head Screw M3x25 1.step',
/* time_stamp */ '2026-10-24T18:52:33-07:00',
/* author */ (''),
/* organization */ (''),
/* preprocessor_version */ 'ST-DEVELOPER v20.2',
/* originating_system */ 'Autodesk Translation Framework v15.17.0.0',
/* authorisation */ '');

FILE_SCHEMA (('AP242_MANAGED_MODEL_BASED_3D_ENGINEERING_MIM_LF { 1 0 10303 442 2 1 4 }'));
ENDSEC;

DATA;
#10=MECHANICAL_DESIGN_GEOMETRIC_PRESENTATION_REPRESENTATION('',(#446),#34876);
#155=SPHERICAL_SURFACE('',#22193,0.005);
#158=(
BOUNDED_CURVE()
B_SPLINE_CURVE(2,(#34461,#34462,#34463),.UNSPECIFIED.,.F.,.F.)
B_SPLINE_CURVE_WITH_KNOTS((3,3),(0.0607926731753692,0.157120419745457),
 .UNSPECIFIED.)
CURVE()
GEOMETRIC_REPRESENTATION_ITEM()
RATIONAL_B_SPLINE_CURVE((1.16988778338128,1.27990737092129,1.3120427295614))
REPRESENTATION_ITEM('')
);
#159=(
BOUNDED_CURVE()
B_SPLINE_CURVE(2,(#34466,#34467,#34468),.UNSPECIFIED.,.F.,.F.)
B_SPLINE_CURVE_WITH_KNOTS((3,3),(0.236610881719778,0.332938628428626),
 .UNSPECIFIED.)
CURVE()
GEOMETRIC_REPRESENTATION_ITEM()
RATIONAL_B_SPLINE_CURVE((1.3120427260588,1.27990736807416,1.16988778190421))
REPRESENTATION_ITEM('')
);
#160=(
BOUNDED_CURVE()
B_SPLINE_CURVE(2,(#34498,#34499,#34500),.UNSPECIFIED.,.F.,.F.)
B_SPLINE_CURVE_WITH_KNOTS((3,3),(0.060792673372948,0.15712042005291),
 .UNSPECIFIED.)
CURVE()
GEOMETRIC_REPRESENTATION_ITEM()
RATIONAL_B_SPLINE_CURVE((1.16988778221416,1.2799073686718,1.31204272679384))
REPRESENTATION_ITEM('')
);
#161=(
BOUNDED_CURVE()
B_SPLINE_CURVE(2,(#34503,#34504,#34505),.UNSPECIFIED.,.F.,.F.)
B_SPLINE_CURVE_WITH_KNOTS((3,3),(0.236610881752925,0.332938628449716),
 .UNSPECIFIED.)
CURVE()
GEOMETRIC_REPRESENTATION_ITEM()
RATIONAL_B_SPLINE_CURVE((1.3120427263507,1.27990736831095,1.16988778202699))
REPRESENTATION_ITEM('')
);
#162=(
BOUNDED_CURVE()
B_SPLINE_CURVE(2,(#34535,#34536,#34537),.UNSPECIFIED.,.F.,.F.)
B_SPLINE_CURVE_WITH_KNOTS((3,3),(0.0607926734092304,0.157120420109433),
 .UNSPECIFIED.)
CURVE()
GEOMETRIC_REPRESENTATION_ITEM()
RATIONAL_B_SPLINE_CURVE((1.1698877820014,1.27990736826137,1.31204272628854))
REPRESENTATION_ITEM('')
);
#163=(
BOUNDED_CURVE()
B_SPLINE_CURVE(2,(#34542,#34543,#34544),.UNSPECIFIED.,.F.,.F.)
B_SPLINE_CURVE_WITH_KNOTS((3,3),(0.23661088156082,0.33293862832676),
 .UNSPECIFIED.)
CURVE()
GEOMETRIC_REPRESENTATION_ITEM()
RATIONAL_B_SPLINE_CURVE((1.31204272463436,1.27990736691681,1.16988778130364))
REPRESENTATION_ITEM('')
);
#164=(
BOUNDED_CURVE()
B_SPLINE_CURVE(2,(#34574,#34575,#34576),.UNSPECIFIED.,.F.,.F.)
B_SPLINE_CURVE_WITH_KNOTS((3,3),(0.0607926733478611,0.157120420013774),
 .UNSPECIFIED.)
CURVE()
GEOMETRIC_REPRESENTATION_ITEM()
RATIONAL_B_SPLINE_CURVE((1.16988778236303,1.27990736895843,1.31204272714642))
REPRESENTATION_ITEM('')
);
#165=(
BOUNDED_CURVE()
B_SPLINE_CURVE(2,(#34579,#34580,#34581),.UNSPECIFIED.,.F.,.F.)
B_SPLINE_CURVE_WITH_KNOTS((3,3),(0.236610882341047,0.332938628827773),
 .UNSPECIFIED.)
CURVE()
GEOMETRIC_REPRESENTATION_ITEM()
RATIONAL_B_SPLINE_CURVE((1.3120427316459,1.27990737261498,1.16988778425995))
REPRESENTATION_ITEM('')
);
#166=(
BOUNDED_CURVE()
B_SPLINE_CURVE(2,(#34671,#34672,#34673),.UNSPECIFIED.,.F.,.F.)
B_SPLINE_CURVE_WITH_KNOTS((3,3),(0.167664209749899,0.177304440757115),
 .UNSPECIFIED.)
CURVE()
GEOMETRIC_REPRESENTATION_ITEM()
RATIONAL_B_SPLINE_CURVE((1.60521077046129,1.32000436275842,1.))
REPRESENTATION_ITEM('')
);
#167=(
BOUNDED_CURVE()
B_SPLINE_CURVE(2,(#34677,#34678,#34679),.UNSPECIFIED.,.F.,.F.)
B_SPLINE_CURVE_WITH_KNOTS((3,3),(0.,0.0096402310072164),.UNSPECIFIED.)
CURVE()
GEOMETRIC_REPRESENTATION_ITEM()
RATIONAL_B_SPLINE_CURVE((1.,1.32000436275842,1.60521077046128))
REPRESENTATION_ITEM('')
);
#168=(
BOUNDED_CURVE()
B_SPLINE_CURVE(2,(#34699,#34700,#34701),.UNSPECIFIED.,.F.,.F.)
B_SPLINE_CURVE_WITH_KNOTS((3,3),(0.167664209749899,0.177304440757115),
 .UNSPECIFIED.)
CURVE()
GEOMETRIC_REPRESENTATION_ITEM()
RATIONAL_B_SPLINE_CURVE((1.60521077046129,1.32000436275842,1.))
REPRESENTATION_ITEM('')
);
#169=(
BOUNDED_CURVE()
B_SPLINE_CURVE(2,(#34704,#34705,#34706),.UNSPECIFIED.,.F.,.F.)
B_SPLINE_CURVE_WITH_KNOTS((3,3),(0.167664209749899,0.177304440757115),
 .UNSPECIFIED.)
CURVE()
GEOMETRIC_REPRESENTATION_ITEM()
RATIONAL_B_SPLINE_CURVE((1.60521077046128,1.32000436275842,1.))
REPRESENTATION_ITEM('')
);
#170=(
BOUNDED_CURVE()
B_SPLINE_CURVE(2,(#34708,#34709,#34710),.UNSPECIFIED.,.F.,.F.)
B_SPLINE_CURVE_WITH_KNOTS((3,3),(0.,0.00964023100721641),.UNSPECIFIED.)
CURVE()
GEOMETRIC_REPRESENTATION_ITEM()
RATIONAL_B_SPLINE_CURVE((1.,1.32000436275842,1.60521077046128))
REPRESENTATION_ITEM('')
);
#171=(
BOUNDED_CURVE()
B_SPLINE_CURVE(2,(#34713,#34714,#34715),.UNSPECIFIED.,.F.,.F.)
B_SPLINE_CURVE_WITH_KNOTS((3,3),(0.167664209749899,0.177304440757115),
 .UNSPECIFIED.)
CURVE()
GEOMETRIC_REPRESENTATION_ITEM()
RATIONAL_B_SPLINE_CURVE((1.60521077046128,1.32000436275842,1.))
REPRESENTATION_ITEM('')
);
#172=(
BOUNDED_CURVE()
B_SPLINE_CURVE(2,(#34720,#34721,#34722),.UNSPECIFIED.,.F.,.F.)
B_SPLINE_CURVE_WITH_KNOTS((3,3),(0.,0.00964023100721641),.UNSPECIFIED.)
CURVE()
GEOMETRIC_REPRESENTATION_ITEM()
RATIONAL_B_SPLINE_CURVE((1.,1.32000436275842,1.60521077046128))
REPRESENTATION_ITEM('')
);
#173=(
BOUNDED_CURVE()
B_SPLINE_CURVE(2,(#34756,#34757,#34758),.UNSPECIFIED.,.F.,.F.)
B_SPLINE_CURVE_WITH_KNOTS((3,3),(0.,0.0096402310072164),.UNSPECIFIED.)
CURVE()
GEOMETRIC_REPRESENTATION_ITEM()
RATIONAL_B_SPLINE_CURVE((1.,1.32000436275842,1.60521077046128))
REPRESENTATION_ITEM('')
);
#188=CONICAL_SURFACE('',#22160,0.0013466375,0.785235177497158);
#189=CONICAL_SURFACE('',#22170,0.00111007998137123,0.462512251778497);
#190=CONICAL_SURFACE('',#22175,0.00111007998137123,0.462512251778497);
#191=CONICAL_SURFACE('',#22180,0.00111007998137123,0.462512251778497);
#192=CONICAL_SURFACE('',#22186,0.00111007998137123,0.462512251778497);
#193=CONICAL_SURFACE('',#22202,0.00277242641351798,0.0349065850398864);
#194=CONICAL_SURFACE('',#22204,0.000209529102193857,0.0872664625997164);
#195=CONICAL_SURFACE('',#22207,0.000209529102193857,0.0872664625997164);
#196=CONICAL_SURFACE('',#22213,0.000209529102193857,0.0872664625997164);
#197=CONICAL_SURFACE('',#22214,0.000209529102193857,0.0872664625997164);
#198=CONICAL_SURFACE('',#22216,0.000409956151237738,1.08210413623649);
#199=CONICAL_SURFACE('',#22221,0.0014323425,0.415478851838033);
#220=B_SPLINE_CURVE_WITH_KNOTS('',3,(#34435,#34436,#34437,#34438,#34439,
#34440,#34441,#34442,#34443,#34444),.UNSPECIFIED.,.F.,.F.,(4,2,2,2,4),(0.0294844094794275,
0.0320672178808003,0.0352683618118342,0.0385150894591433,0.0409598490463399),
 .UNSPECIFIED.);
#221=B_SPLINE_CURVE_WITH_KNOTS('',3,(#34448,#34449,#34450,#34451,#34452,
#34453,#34454,#34455,#34456,#34457),.UNSPECIFIED.,.F.,.F.,(4,2,2,2,4),(0.0104731770181891,
0.0129179366053853,0.0161646642526944,0.0193658081837281,0.0219486165852225),
 .UNSPECIFIED.);
#222=B_SPLINE_CURVE_WITH_KNOTS('',3,(#34472,#34473,#34474,#34475,#34476,
#34477,#34478,#34479,#34480,#34481),.UNSPECIFIED.,.F.,.F.,(4,2,2,2,4),(0.0294844112755818,
0.0320672196769547,0.0352683636079885,0.0385150912552978,0.0409598508424944),
 .UNSPECIFIED.);
#223=B_SPLINE_CURVE_WITH_KNOTS('',3,(#34485,#34486,#34487,#34488,#34489,
#34490,#34491,#34492,#34493,#34494),.UNSPECIFIED.,.F.,.F.,(4,2,2,2,4),(0.0104731770181892,
0.0129179366053856,0.0161646642526945,0.0193658081837283,0.0219486165852223),
 .UNSPECIFIED.);
#224=B_SPLINE_CURVE_WITH_KNOTS('',3,(#34509,#34510,#34511,#34512,#34513,
#34514,#34515,#34516,#34517,#34518),.UNSPECIFIED.,.F.,.F.,(4,2,2,2,4),(0.0294844112754596,
0.0320672196769543,0.0352683636079882,0.0385150912552974,0.040959850842494),
 .UNSPECIFIED.);
#225=B_SPLINE_CURVE_WITH_KNOTS('',3,(#34522,#34523,#34524,#34525,#34526,
#34527,#34528,#34529,#34530,#34531),.UNSPECIFIED.,.F.,.F.,(4,2,2,2,4),(0.0104731770181891,
0.0129179366053853,0.0161646642526943,0.0193658081837282,0.0219486165851014),
 .UNSPECIFIED.);
#226=B_SPLINE_CURVE_WITH_KNOTS('',3,(#34548,#34549,#34550,#34551,#34552,
#34553,#34554,#34555,#34556,#34557),.UNSPECIFIED.,.F.,.F.,(4,2,2,2,4),(0.029484409479306,
0.0320672178808001,0.0352683618118339,0.038515089459143,0.0409598490463398),
 .UNSPECIFIED.);
#227=B_SPLINE_CURVE_WITH_KNOTS('',3,(#34561,#34562,#34563,#34564,#34565,
#34566,#34567,#34568,#34569,#34570),.UNSPECIFIED.,.F.,.F.,(4,2,2,2,4),(0.0104731770181892,
0.0129179366053856,0.0161646642526945,0.0193658081837283,0.0219486165851011),
 .UNSPECIFIED.);
#228=B_SPLINE_CURVE_WITH_KNOTS('',3,(#34594,#34595,#34596,#34597,#34598,
#34599,#34600,#34601,#34602,#34603),.UNSPECIFIED.,.F.,.F.,(4,2,2,2,4),(0.0992219002317977,
0.105487377923686,0.113471050376119,0.121445475099517,0.129419899822916),
 .UNSPECIFIED.);
#229=B_SPLINE_CURVE_WITH_KNOTS('',3,(#34608,#34609,#34610,#34611,#34612,
#34613,#34614,#34615,#34616,#34617),.UNSPECIFIED.,.F.,.F.,(4,2,2,2,4),(0.0992219004931051,
0.105487378184993,0.113471050637426,0.121445475360824,0.129419900084223),
 .UNSPECIFIED.);
#230=B_SPLINE_CURVE_WITH_KNOTS('',3,(#34622,#34623,#34624,#34625,#34626,
#34627,#34628,#34629,#34630,#34631),.UNSPECIFIED.,.F.,.F.,(4,2,2,2,4),(0.099221900231798,
0.105487377923686,0.113471050376119,0.121445475099517,0.129419899822916),
 .UNSPECIFIED.);
#231=B_SPLINE_CURVE_WITH_KNOTS('',3,(#34636,#34637,#34638,#34639,#34640,
#34641,#34642,#34643,#34644,#34645),.UNSPECIFIED.,.F.,.F.,(4,2,2,2,4),(0.0992219004931048,
0.105487378184993,0.113471050637426,0.121445475360825,0.129419900084223),
 .UNSPECIFIED.);
#232=B_SPLINE_CURVE_WITH_KNOTS('',3,(#34655,#34656,#34657,#34658,#34659,
#34660,#34661,#34662,#34663,#34664,#34665,#34666,#34667,#34668),
 .UNSPECIFIED.,.F.,.F.,(4,2,2,2,2,2,4),(0.00869408947528055,0.0191036740231402,
0.0270432080340005,0.0349827420448608,0.0429222760557212,0.0508618100665816,
0.0612713946144406),.UNSPECIFIED.);
#233=B_SPLINE_CURVE_WITH_KNOTS('',3,(#34683,#34684,#34685,#34686,#34687,
#34688,#34689,#34690,#34691,#34692,#34693,#34694,#34695,#34696),
 .UNSPECIFIED.,.F.,.F.,(4,2,2,2,2,2,4),(0.00869408947528055,0.0191036740231402,
0.0270432080340005,0.0349827420448608,0.0429222760557211,0.0508618100665814,
0.061271394614441),.UNSPECIFIED.);
#234=B_SPLINE_CURVE_WITH_KNOTS('',3,(#34724,#34725,#34726,#34727,#34728,
#34729,#34730,#34731,#34732,#34733,#34734,#34735,#34736,#34737),
 .UNSPECIFIED.,.F.,.F.,(4,2,2,2,2,2,4),(0.00869408947528073,0.0191036740231402,
0.0270432080340005,0.0349827420448608,0.0429222760557212,0.0508618100665817,
0.0612713946144409),.UNSPECIFIED.);
#235=B_SPLINE_CURVE_WITH_KNOTS('',3,(#34740,#34741,#34742,#34743,#34744,
#34745,#34746,#34747,#34748,#34749,#34750,#34751,#34752,#34753),
 .UNSPECIFIED.,.F.,.F.,(4,2,2,2,2,2,4),(0.00869408947528071,0.0191036740231402,
0.0270432080340005,0.0349827420448608,0.0429222760557211,0.0508618100665814,
0.0612713946144409),.UNSPECIFIED.);
#380=SHAPE_REPRESENTATION_RELATIONSHIP('SRR','None',#35017,#413);
#413=ADVANCED_BREP_SHAPE_REPRESENTATION('',(#479),#34875);
#446=STYLED_ITEM('',(#35164),#479);
#479=MANIFOLD_SOLID_BREP('Pan Head Screw M3x25 1',#19586);
#588=FACE_BOUND('',#6974,.T.);
#589=FACE_BOUND('',#6991,.T.);
#1073=PLANE('',#22166);
#1074=PLANE('',#22205);
#1075=PLANE('',#22206);
#1076=PLANE('',#22208);
#1077=PLANE('',#22209);
#1078=PLANE('',#22210);
#1079=PLANE('',#22211);
#1080=PLANE('',#22212);
#1081=PLANE('',#22215);
#1082=PLANE('',#22220);
#2668=LINE('',#34424,#4267);
#2669=LINE('',#34429,#4268);
#2670=LINE('',#34650,#4269);
#2671=LINE('',#34653,#4270);
#2672=LINE('',#34669,#4271);
#2673=LINE('',#34676,#4272);
#2674=LINE('',#34682,#4273);
#2675=LINE('',#34702,#4274);
#2676=LINE('',#34716,#4275);
#2677=LINE('',#34719,#4276);
#2678=LINE('',#34754,#4277);
#2679=LINE('',#34761,#4278);
#2680=LINE('',#34766,#4279);
#2681=LINE('',#34770,#4280);
#4267=VECTOR('',#28265,0.0013466375);
#4268=VECTOR('',#28272,0.0015);
#4269=VECTOR('',#28351,0.00277242641351798);
#4270=VECTOR('',#28354,1.);
#4271=VECTOR('',#28355,1.);
#4272=VECTOR('',#28360,1.);
#4273=VECTOR('',#28363,1.);
#4274=VECTOR('',#28366,1.);
#4275=VECTOR('',#28373,1.);
#4276=VECTOR('',#28376,1.);
#4277=VECTOR('',#28381,1.);
#4278=VECTOR('',#28386,0.000409956151237738);
#4279=VECTOR('',#28391,0.001364685);
#4280=VECTOR('',#28398,0.0014323425);
#4791=CYLINDRICAL_SURFACE('',#22164,0.0015);
#4792=CYLINDRICAL_SURFACE('',#22217,0.001364685);
#5808=FACE_OUTER_BOUND('',#6961,.T.);
#5809=FACE_OUTER_BOUND('',#6962,.T.);
#5810=FACE_OUTER_BOUND('',#6963,.T.);
#5811=FACE_OUTER_BOUND('',#6964,.T.);
#5812=FACE_OUTER_BOUND('',#6965,.T.);
#5813=FACE_OUTER_BOUND('',#6966,.T.);
#5814=FACE_OUTER_BOUND('',#6967,.T.);
#5815=FACE_OUTER_BOUND('',#6968,.T.);
#5816=FACE_OUTER_BOUND('',#6969,.T.);
#5817=FACE_OUTER_BOUND('',#6970,.T.);
#5818=FACE_OUTER_BOUND('',#6971,.T.);
#5819=FACE_OUTER_BOUND('',#6972,.T.);
#5820=FACE_OUTER_BOUND('',#6973,.T.);
#5821=FACE_OUTER_BOUND('',#6975,.T.);
#5822=FACE_OUTER_BOUND('',#6976,.T.);
#5823=FACE_OUTER_BOUND('',#6977,.T.);
#5824=FACE_OUTER_BOUND('',#6978,.T.);
#5825=FACE_OUTER_BOUND('',#6979,.T.);
#5826=FACE_OUTER_BOUND('',#6980,.T.);
#5827=FACE_OUTER_BOUND('',#6981,.T.);
#5828=FACE_OUTER_BOUND('',#6982,.T.);
#5829=FACE_OUTER_BOUND('',#6983,.T.);
#5830=FACE_OUTER_BOUND('',#6984,.T.);
#5831=FACE_OUTER_BOUND('',#6985,.T.);
#5832=FACE_OUTER_BOUND('',#6986,.T.);
#5833=FACE_OUTER_BOUND('',#6987,.T.);
#5834=FACE_OUTER_BOUND('',#6988,.T.);
#5835=FACE_OUTER_BOUND('',#6989,.T.);
#5836=FACE_OUTER_BOUND('',#6990,.T.);
#5837=FACE_OUTER_BOUND('',#6992,.T.);
#6961=EDGE_LOOP('',(#18340,#18341,#18342,#18343,#18344));
#6962=EDGE_LOOP('',(#18345,#18346,#18347,#18348,#18349));
#6963=EDGE_LOOP('',(#18350));
#6964=EDGE_LOOP('',(#18351,#18352,#18353,#18354));
#6965=EDGE_LOOP('',(#18355,#18356,#18357,#18358));
#6966=EDGE_LOOP('',(#18359,#18360,#18361,#18362));
#6967=EDGE_LOOP('',(#18363,#18364,#18365,#18366));
#6968=EDGE_LOOP('',(#18367,#18368,#18369,#18370));
#6969=EDGE_LOOP('',(#18371,#18372,#18373,#18374,#18375));
#6970=EDGE_LOOP('',(#18376,#18377,#18378,#18379));
#6971=EDGE_LOOP('',(#18380,#18381,#18382,#18383));
#6972=EDGE_LOOP('',(#18384,#18385,#18386,#18387,#18388));
#6973=EDGE_LOOP('',(#18389));
#6974=EDGE_LOOP('',(#18390,#18391,#18392,#18393,#18394,#18395,#18396,#18397,
#18398,#18399,#18400,#18401,#18402,#18403,#18404,#18405));
#6975=EDGE_LOOP('',(#18406,#18407,#18408,#18409,#18410));
#6976=EDGE_LOOP('',(#18411,#18412,#18413,#18414));
#6977=EDGE_LOOP('',(#18415,#18416,#18417,#18418,#18419));
#6978=EDGE_LOOP('',(#18420,#18421,#18422,#18423,#18424));
#6979=EDGE_LOOP('',(#18425,#18426,#18427,#18428));
#6980=EDGE_LOOP('',(#18429,#18430,#18431,#18432,#18433));
#6981=EDGE_LOOP('',(#18434,#18435,#18436,#18437,#18438));
#6982=EDGE_LOOP('',(#18439,#18440,#18441,#18442,#18443));
#6983=EDGE_LOOP('',(#18444,#18445,#18446,#18447,#18448));
#6984=EDGE_LOOP('',(#18449,#18450,#18451,#18452,#18453));
#6985=EDGE_LOOP('',(#18454,#18455,#18456,#18457));
#6986=EDGE_LOOP('',(#18458,#18459,#18460,#18461));
#6987=EDGE_LOOP('',(#18462,#18463,#18464,#18465,#18466));
#6988=EDGE_LOOP('',(#18467,#18468,#18469,#18470,#18471,#18472,#18473,#18474,
#18475,#18476,#18477,#18478,#18479,#18480,#18481,#18482,#18483,#18484,#18485));
#6989=EDGE_LOOP('',(#18486,#18487,#18488,#18489));
#6990=EDGE_LOOP('',(#18490));
#6991=EDGE_LOOP('',(#18491));
#6992=EDGE_LOOP('',(#18492,#18493,#18494,#18495));
#8041=CIRCLE('',#22161,0.00150000000001);
#8042=CIRCLE('',#22162,0.00119327500001);
#8043=CIRCLE('',#22163,0.00150000000001);
#8044=CIRCLE('',#22165,0.00150000000001);
#8045=CIRCLE('',#22168,0.00136794617523955);
#8046=CIRCLE('',#22169,0.00147019793481599);
#8047=CIRCLE('',#22171,0.000819912302485476);
#8048=CIRCLE('',#22173,0.00136794617523955);
#8049=CIRCLE('',#22174,0.00147019793481599);
#8050=CIRCLE('',#22176,0.000819912302485476);
#8051=CIRCLE('',#22178,0.00136794617523955);
#8052=CIRCLE('',#22179,0.00147019793481599);
#8053=CIRCLE('',#22181,0.000819912302485476);
#8054=CIRCLE('',#22182,0.000819912302485476);
#8055=CIRCLE('',#22184,0.00136794617523955);
#8056=CIRCLE('',#22185,0.00147019793481599);
#8057=CIRCLE('',#22187,0.000819912302485476);
#8058=CIRCLE('',#22189,0.0027642230121603);
#8059=CIRCLE('',#22190,0.001);
#8060=CIRCLE('',#22191,0.002206040231424);
#8061=CIRCLE('',#22192,0.0027642230121603);
#8062=CIRCLE('',#22194,0.0049973967301825);
#8063=CIRCLE('',#22195,0.0049973967301825);
#8064=CIRCLE('',#22196,0.0049973967301825);
#8065=CIRCLE('',#22197,0.0049973967301825);
#8066=CIRCLE('',#22198,0.0049973967301825);
#8067=CIRCLE('',#22199,0.0049973967301825);
#8068=CIRCLE('',#22200,0.0049973967301825);
#8069=CIRCLE('',#22201,0.0049973967301825);
#8070=CIRCLE('',#22203,0.00280000000001);
#8071=CIRCLE('',#22218,0.00136468500001);
#8072=CIRCLE('',#22219,0.00136468500001);
#9909=VERTEX_POINT('',#34420);
#9910=VERTEX_POINT('',#34421);
#9911=VERTEX_POINT('',#34423);
#9912=VERTEX_POINT('',#34428);
#9913=VERTEX_POINT('',#34433);
#9914=VERTEX_POINT('',#34434);
#9915=VERTEX_POINT('',#34445);
#9916=VERTEX_POINT('',#34447);
#9917=VERTEX_POINT('',#34460);
#9918=VERTEX_POINT('',#34464);
#9919=VERTEX_POINT('',#34470);
#9920=VERTEX_POINT('',#34471);
#9921=VERTEX_POINT('',#34482);
#9922=VERTEX_POINT('',#34484);
#9923=VERTEX_POINT('',#34497);
#9924=VERTEX_POINT('',#34501);
#9925=VERTEX_POINT('',#34507);
#9926=VERTEX_POINT('',#34508);
#9927=VERTEX_POINT('',#34519);
#9928=VERTEX_POINT('',#34521);
#9929=VERTEX_POINT('',#34534);
#9930=VERTEX_POINT('',#34538);
#9931=VERTEX_POINT('',#34540);
#9932=VERTEX_POINT('',#34546);
#9933=VERTEX_POINT('',#34547);
#9934=VERTEX_POINT('',#34558);
#9935=VERTEX_POINT('',#34560);
#9936=VERTEX_POINT('',#34573);
#9937=VERTEX_POINT('',#34577);
#9938=VERTEX_POINT('',#34583);
#9939=VERTEX_POINT('',#34584);
#9940=VERTEX_POINT('',#34586);
#9941=VERTEX_POINT('',#34591);
#9942=VERTEX_POINT('',#34593);
#9943=VERTEX_POINT('',#34605);
#9944=VERTEX_POINT('',#34607);
#9945=VERTEX_POINT('',#34619);
#9946=VERTEX_POINT('',#34621);
#9947=VERTEX_POINT('',#34633);
#9948=VERTEX_POINT('',#34635);
#9949=VERTEX_POINT('',#34648);
#9950=VERTEX_POINT('',#34652);
#9951=VERTEX_POINT('',#34654);
#9952=VERTEX_POINT('',#34675);
#9953=VERTEX_POINT('',#34681);
#9954=VERTEX_POINT('',#34698);
#9955=VERTEX_POINT('',#34712);
#9956=VERTEX_POINT('',#34718);
#9957=VERTEX_POINT('',#34739);
#9958=VERTEX_POINT('',#34760);
#9959=VERTEX_POINT('',#34763);
#9960=VERTEX_POINT('',#34765);
#12728=EDGE_CURVE('',#9909,#9910,#8041,.T.);
#12729=EDGE_CURVE('',#9910,#9911,#2668,.T.);
#12730=EDGE_CURVE('',#9911,#9911,#8042,.T.);
#12731=EDGE_CURVE('',#9910,#9909,#8043,.T.);
#12732=EDGE_CURVE('',#9909,#9912,#2669,.T.);
#12733=EDGE_CURVE('',#9912,#9912,#8044,.T.);
#12734=EDGE_CURVE('',#9913,#9914,#220,.F.);
#12735=EDGE_CURVE('',#9914,#9915,#8045,.T.);
#12736=EDGE_CURVE('',#9915,#9916,#221,.F.);
#12737=EDGE_CURVE('',#9916,#9913,#8046,.T.);
#12738=EDGE_CURVE('',#9914,#9917,#158,.T.);
#12739=EDGE_CURVE('',#9917,#9918,#8047,.T.);
#12740=EDGE_CURVE('',#9918,#9915,#159,.T.);
#12741=EDGE_CURVE('',#9919,#9920,#222,.F.);
#12742=EDGE_CURVE('',#9920,#9921,#8048,.T.);
#12743=EDGE_CURVE('',#9921,#9922,#223,.F.);
#12744=EDGE_CURVE('',#9922,#9919,#8049,.T.);
#12745=EDGE_CURVE('',#9920,#9923,#160,.T.);
#12746=EDGE_CURVE('',#9923,#9924,#8050,.T.);
#12747=EDGE_CURVE('',#9924,#9921,#161,.T.);
#12748=EDGE_CURVE('',#9925,#9926,#224,.F.);
#12749=EDGE_CURVE('',#9926,#9927,#8051,.T.);
#12750=EDGE_CURVE('',#9927,#9928,#225,.F.);
#12751=EDGE_CURVE('',#9928,#9925,#8052,.T.);
#12752=EDGE_CURVE('',#9926,#9929,#162,.T.);
#12753=EDGE_CURVE('',#9929,#9930,#8053,.T.);
#12754=EDGE_CURVE('',#9930,#9931,#8054,.T.);
#12755=EDGE_CURVE('',#9931,#9927,#163,.T.);
#12756=EDGE_CURVE('',#9932,#9933,#226,.F.);
#12757=EDGE_CURVE('',#9933,#9934,#8055,.T.);
#12758=EDGE_CURVE('',#9934,#9935,#227,.F.);
#12759=EDGE_CURVE('',#9935,#9932,#8056,.T.);
#12760=EDGE_CURVE('',#9933,#9936,#164,.T.);
#12761=EDGE_CURVE('',#9936,#9937,#8057,.T.);
#12762=EDGE_CURVE('',#9937,#9934,#165,.T.);
#12763=EDGE_CURVE('',#9938,#9939,#8058,.T.);
#12764=EDGE_CURVE('',#9939,#9940,#8059,.T.);
#12765=EDGE_CURVE('',#9940,#9940,#8060,.T.);
#12766=EDGE_CURVE('',#9939,#9938,#8061,.T.);
#12767=EDGE_CURVE('',#9941,#9916,#8062,.T.);
#12768=EDGE_CURVE('',#9942,#9941,#228,.F.);
#12769=EDGE_CURVE('',#9932,#9942,#8063,.T.);
#12770=EDGE_CURVE('',#9943,#9935,#8064,.T.);
#12771=EDGE_CURVE('',#9944,#9943,#229,.F.);
#12772=EDGE_CURVE('',#9925,#9944,#8065,.T.);
#12773=EDGE_CURVE('',#9945,#9928,#8066,.T.);
#12774=EDGE_CURVE('',#9946,#9945,#230,.F.);
#12775=EDGE_CURVE('',#9919,#9946,#8067,.T.);
#12776=EDGE_CURVE('',#9947,#9922,#8068,.T.);
#12777=EDGE_CURVE('',#9948,#9947,#231,.F.);
#12778=EDGE_CURVE('',#9913,#9948,#8069,.T.);
#12779=EDGE_CURVE('',#9949,#9949,#8070,.T.);
#12780=EDGE_CURVE('',#9949,#9938,#2670,.T.);
#12781=EDGE_CURVE('',#9941,#9950,#2671,.T.);
#12782=EDGE_CURVE('',#9951,#9950,#232,.F.);
#12783=EDGE_CURVE('',#9942,#9951,#2672,.T.);
#12784=EDGE_CURVE('',#9950,#9918,#166,.T.);
#12785=EDGE_CURVE('',#9948,#9952,#2673,.T.);
#12786=EDGE_CURVE('',#9917,#9952,#167,.T.);
#12787=EDGE_CURVE('',#9947,#9953,#2674,.T.);
#12788=EDGE_CURVE('',#9952,#9953,#233,.F.);
#12789=EDGE_CURVE('',#9954,#9931,#168,.T.);
#12790=EDGE_CURVE('',#9945,#9954,#2675,.T.);
#12791=EDGE_CURVE('',#9953,#9924,#169,.T.);
#12792=EDGE_CURVE('',#9936,#9951,#170,.T.);
#12793=EDGE_CURVE('',#9955,#9937,#171,.T.);
#12794=EDGE_CURVE('',#9943,#9955,#2676,.T.);
#12795=EDGE_CURVE('',#9946,#9956,#2677,.T.);
#12796=EDGE_CURVE('',#9923,#9956,#172,.T.);
#12797=EDGE_CURVE('',#9956,#9954,#234,.F.);
#12798=EDGE_CURVE('',#9957,#9955,#235,.F.);
#12799=EDGE_CURVE('',#9944,#9957,#2678,.T.);
#12800=EDGE_CURVE('',#9929,#9957,#173,.T.);
#12801=EDGE_CURVE('',#9958,#9930,#2679,.T.);
#12802=EDGE_CURVE('',#9959,#9959,#8071,.T.);
#12803=EDGE_CURVE('',#9959,#9960,#2680,.T.);
#12804=EDGE_CURVE('',#9960,#9960,#8072,.T.);
#12805=EDGE_CURVE('',#9912,#9959,#2681,.T.);
#18340=ORIENTED_EDGE('',*,*,#12728,.T.);
#18341=ORIENTED_EDGE('',*,*,#12729,.T.);
#18342=ORIENTED_EDGE('',*,*,#12730,.T.);
#18343=ORIENTED_EDGE('',*,*,#12729,.F.);
#18344=ORIENTED_EDGE('',*,*,#12731,.T.);
#18345=ORIENTED_EDGE('',*,*,#12728,.F.);
#18346=ORIENTED_EDGE('',*,*,#12732,.T.);
#18347=ORIENTED_EDGE('',*,*,#12733,.T.);
#18348=ORIENTED_EDGE('',*,*,#12732,.F.);
#18349=ORIENTED_EDGE('',*,*,#12731,.F.);
#18350=ORIENTED_EDGE('',*,*,#12730,.F.);
#18351=ORIENTED_EDGE('',*,*,#12734,.T.);
#18352=ORIENTED_EDGE('',*,*,#12735,.T.);
#18353=ORIENTED_EDGE('',*,*,#12736,.T.);
#18354=ORIENTED_EDGE('',*,*,#12737,.T.);
#18355=ORIENTED_EDGE('',*,*,#12735,.F.);
#18356=ORIENTED_EDGE('',*,*,#12738,.T.);
#18357=ORIENTED_EDGE('',*,*,#12739,.T.);
#18358=ORIENTED_EDGE('',*,*,#12740,.T.);
#18359=ORIENTED_EDGE('',*,*,#12741,.T.);
#18360=ORIENTED_EDGE('',*,*,#12742,.T.);
#18361=ORIENTED_EDGE('',*,*,#12743,.T.);
#18362=ORIENTED_EDGE('',*,*,#12744,.T.);
#18363=ORIENTED_EDGE('',*,*,#12742,.F.);
#18364=ORIENTED_EDGE('',*,*,#12745,.T.);
#18365=ORIENTED_EDGE('',*,*,#12746,.T.);
#18366=ORIENTED_EDGE('',*,*,#12747,.T.);
#18367=ORIENTED_EDGE('',*,*,#12748,.T.);
#18368=ORIENTED_EDGE('',*,*,#12749,.T.);
#18369=ORIENTED_EDGE('',*,*,#12750,.T.);
#18370=ORIENTED_EDGE('',*,*,#12751,.T.);
#18371=ORIENTED_EDGE('',*,*,#12749,.F.);
#18372=ORIENTED_EDGE('',*,*,#12752,.T.);
#18373=ORIENTED_EDGE('',*,*,#12753,.T.);
#18374=ORIENTED_EDGE('',*,*,#12754,.T.);
#18375=ORIENTED_EDGE('',*,*,#12755,.T.);
#18376=ORIENTED_EDGE('',*,*,#12756,.T.);
#18377=ORIENTED_EDGE('',*,*,#12757,.T.);
#18378=ORIENTED_EDGE('',*,*,#12758,.T.);
#18379=ORIENTED_EDGE('',*,*,#12759,.T.);
#18380=ORIENTED_EDGE('',*,*,#12757,.F.);
#18381=ORIENTED_EDGE('',*,*,#12760,.T.);
#18382=ORIENTED_EDGE('',*,*,#12761,.T.);
#18383=ORIENTED_EDGE('',*,*,#12762,.T.);
#18384=ORIENTED_EDGE('',*,*,#12763,.T.);
#18385=ORIENTED_EDGE('',*,*,#12764,.T.);
#18386=ORIENTED_EDGE('',*,*,#12765,.T.);
#18387=ORIENTED_EDGE('',*,*,#12764,.F.);
#18388=ORIENTED_EDGE('',*,*,#12766,.T.);
#18389=ORIENTED_EDGE('',*,*,#12765,.F.);
#18390=ORIENTED_EDGE('',*,*,#12767,.F.);
#18391=ORIENTED_EDGE('',*,*,#12768,.F.);
#18392=ORIENTED_EDGE('',*,*,#12769,.F.);
#18393=ORIENTED_EDGE('',*,*,#12759,.F.);
#18394=ORIENTED_EDGE('',*,*,#12770,.F.);
#18395=ORIENTED_EDGE('',*,*,#12771,.F.);
#18396=ORIENTED_EDGE('',*,*,#12772,.F.);
#18397=ORIENTED_EDGE('',*,*,#12751,.F.);
#18398=ORIENTED_EDGE('',*,*,#12773,.F.);
#18399=ORIENTED_EDGE('',*,*,#12774,.F.);
#18400=ORIENTED_EDGE('',*,*,#12775,.F.);
#18401=ORIENTED_EDGE('',*,*,#12744,.F.);
#18402=ORIENTED_EDGE('',*,*,#12776,.F.);
#18403=ORIENTED_EDGE('',*,*,#12777,.F.);
#18404=ORIENTED_EDGE('',*,*,#12778,.F.);
#18405=ORIENTED_EDGE('',*,*,#12737,.F.);
#18406=ORIENTED_EDGE('',*,*,#12779,.F.);
#18407=ORIENTED_EDGE('',*,*,#12780,.T.);
#18408=ORIENTED_EDGE('',*,*,#12766,.F.);
#18409=ORIENTED_EDGE('',*,*,#12763,.F.);
#18410=ORIENTED_EDGE('',*,*,#12780,.F.);
#18411=ORIENTED_EDGE('',*,*,#12768,.T.);
#18412=ORIENTED_EDGE('',*,*,#12781,.T.);
#18413=ORIENTED_EDGE('',*,*,#12782,.F.);
#18414=ORIENTED_EDGE('',*,*,#12783,.F.);
#18415=ORIENTED_EDGE('',*,*,#12767,.T.);
#18416=ORIENTED_EDGE('',*,*,#12736,.F.);
#18417=ORIENTED_EDGE('',*,*,#12740,.F.);
#18418=ORIENTED_EDGE('',*,*,#12784,.F.);
#18419=ORIENTED_EDGE('',*,*,#12781,.F.);
#18420=ORIENTED_EDGE('',*,*,#12778,.T.);
#18421=ORIENTED_EDGE('',*,*,#12785,.T.);
#18422=ORIENTED_EDGE('',*,*,#12786,.F.);
#18423=ORIENTED_EDGE('',*,*,#12738,.F.);
#18424=ORIENTED_EDGE('',*,*,#12734,.F.);
#18425=ORIENTED_EDGE('',*,*,#12777,.T.);
#18426=ORIENTED_EDGE('',*,*,#12787,.T.);
#18427=ORIENTED_EDGE('',*,*,#12788,.F.);
#18428=ORIENTED_EDGE('',*,*,#12785,.F.);
#18429=ORIENTED_EDGE('',*,*,#12773,.T.);
#18430=ORIENTED_EDGE('',*,*,#12750,.F.);
#18431=ORIENTED_EDGE('',*,*,#12755,.F.);
#18432=ORIENTED_EDGE('',*,*,#12789,.F.);
#18433=ORIENTED_EDGE('',*,*,#12790,.F.);
#18434=ORIENTED_EDGE('',*,*,#12776,.T.);
#18435=ORIENTED_EDGE('',*,*,#12743,.F.);
#18436=ORIENTED_EDGE('',*,*,#12747,.F.);
#18437=ORIENTED_EDGE('',*,*,#12791,.F.);
#18438=ORIENTED_EDGE('',*,*,#12787,.F.);
#18439=ORIENTED_EDGE('',*,*,#12769,.T.);
#18440=ORIENTED_EDGE('',*,*,#12783,.T.);
#18441=ORIENTED_EDGE('',*,*,#12792,.F.);
#18442=ORIENTED_EDGE('',*,*,#12760,.F.);
#18443=ORIENTED_EDGE('',*,*,#12756,.F.);
#18444=ORIENTED_EDGE('',*,*,#12770,.T.);
#18445=ORIENTED_EDGE('',*,*,#12758,.F.);
#18446=ORIENTED_EDGE('',*,*,#12762,.F.);
#18447=ORIENTED_EDGE('',*,*,#12793,.F.);
#18448=ORIENTED_EDGE('',*,*,#12794,.F.);
#18449=ORIENTED_EDGE('',*,*,#12775,.T.);
#18450=ORIENTED_EDGE('',*,*,#12795,.T.);
#18451=ORIENTED_EDGE('',*,*,#12796,.F.);
#18452=ORIENTED_EDGE('',*,*,#12745,.F.);
#18453=ORIENTED_EDGE('',*,*,#12741,.F.);
#18454=ORIENTED_EDGE('',*,*,#12774,.T.);
#18455=ORIENTED_EDGE('',*,*,#12790,.T.);
#18456=ORIENTED_EDGE('',*,*,#12797,.F.);
#18457=ORIENTED_EDGE('',*,*,#12795,.F.);
#18458=ORIENTED_EDGE('',*,*,#12771,.T.);
#18459=ORIENTED_EDGE('',*,*,#12794,.T.);
#18460=ORIENTED_EDGE('',*,*,#12798,.F.);
#18461=ORIENTED_EDGE('',*,*,#12799,.F.);
#18462=ORIENTED_EDGE('',*,*,#12772,.T.);
#18463=ORIENTED_EDGE('',*,*,#12799,.T.);
#18464=ORIENTED_EDGE('',*,*,#12800,.F.);
#18465=ORIENTED_EDGE('',*,*,#12752,.F.);
#18466=ORIENTED_EDGE('',*,*,#12748,.F.);
#18467=ORIENTED_EDGE('',*,*,#12801,.T.);
#18468=ORIENTED_EDGE('',*,*,#12753,.F.);
#18469=ORIENTED_EDGE('',*,*,#12800,.T.);
#18470=ORIENTED_EDGE('',*,*,#12798,.T.);
#18471=ORIENTED_EDGE('',*,*,#12793,.T.);
#18472=ORIENTED_EDGE('',*,*,#12761,.F.);
#18473=ORIENTED_EDGE('',*,*,#12792,.T.);
#18474=ORIENTED_EDGE('',*,*,#12782,.T.);
#18475=ORIENTED_EDGE('',*,*,#12784,.T.);
#18476=ORIENTED_EDGE('',*,*,#12739,.F.);
#18477=ORIENTED_EDGE('',*,*,#12786,.T.);
#18478=ORIENTED_EDGE('',*,*,#12788,.T.);
#18479=ORIENTED_EDGE('',*,*,#12791,.T.);
#18480=ORIENTED_EDGE('',*,*,#12746,.F.);
#18481=ORIENTED_EDGE('',*,*,#12796,.T.);
#18482=ORIENTED_EDGE('',*,*,#12797,.T.);
#18483=ORIENTED_EDGE('',*,*,#12789,.T.);
#18484=ORIENTED_EDGE('',*,*,#12754,.F.);
#18485=ORIENTED_EDGE('',*,*,#12801,.F.);
#18486=ORIENTED_EDGE('',*,*,#12802,.F.);
#18487=ORIENTED_EDGE('',*,*,#12803,.T.);
#18488=ORIENTED_EDGE('',*,*,#12804,.T.);
#18489=ORIENTED_EDGE('',*,*,#12803,.F.);
#18490=ORIENTED_EDGE('',*,*,#12779,.T.);
#18491=ORIENTED_EDGE('',*,*,#12804,.F.);
#18492=ORIENTED_EDGE('',*,*,#12733,.F.);
#18493=ORIENTED_EDGE('',*,*,#12805,.T.);
#18494=ORIENTED_EDGE('',*,*,#12802,.T.);
#18495=ORIENTED_EDGE('',*,*,#12805,.F.);
#18504=TOROIDAL_SURFACE('',#22167,0.00144491053032732,8.6E-5);
#18505=TOROIDAL_SURFACE('',#22172,0.00144491053032732,8.6E-5);
#18506=TOROIDAL_SURFACE('',#22177,0.00144491053032732,8.6E-5);
#18507=TOROIDAL_SURFACE('',#22183,0.00144491053032732,8.6E-5);
#18508=TOROIDAL_SURFACE('',#22188,0.0017648321851312,0.001);
#19524=ADVANCED_FACE('',(#5808),#188,.T.);
#19525=ADVANCED_FACE('',(#5809),#4791,.T.);
#19526=ADVANCED_FACE('',(#5810),#1073,.T.);
#19527=ADVANCED_FACE('',(#5811),#18504,.T.);
#19528=ADVANCED_FACE('',(#5812),#189,.F.);
#19529=ADVANCED_FACE('',(#5813),#18505,.T.);
#19530=ADVANCED_FACE('',(#5814),#190,.F.);
#19531=ADVANCED_FACE('',(#5815),#18506,.T.);
#19532=ADVANCED_FACE('',(#5816),#191,.F.);
#19533=ADVANCED_FACE('',(#5817),#18507,.T.);
#19534=ADVANCED_FACE('',(#5818),#192,.F.);
#19535=ADVANCED_FACE('',(#5819),#18508,.T.);
#19536=ADVANCED_FACE('',(#5820,#588),#155,.T.);
#19537=ADVANCED_FACE('',(#5821),#193,.T.);
#19538=ADVANCED_FACE('',(#5822),#194,.T.);
#19539=ADVANCED_FACE('',(#5823),#1074,.T.);
#19540=ADVANCED_FACE('',(#5824),#1075,.T.);
#19541=ADVANCED_FACE('',(#5825),#195,.T.);
#19542=ADVANCED_FACE('',(#5826),#1076,.T.);
#19543=ADVANCED_FACE('',(#5827),#1077,.T.);
#19544=ADVANCED_FACE('',(#5828),#1078,.T.);
#19545=ADVANCED_FACE('',(#5829),#1079,.T.);
#19546=ADVANCED_FACE('',(#5830),#1080,.T.);
#19547=ADVANCED_FACE('',(#5831),#196,.T.);
#19548=ADVANCED_FACE('',(#5832),#197,.T.);
#19549=ADVANCED_FACE('',(#5833),#1081,.T.);
#19550=ADVANCED_FACE('',(#5834),#198,.F.);
#19551=ADVANCED_FACE('',(#5835),#4792,.T.);
#19552=ADVANCED_FACE('',(#5836,#589),#1082,.T.);
#19553=ADVANCED_FACE('',(#5837),#199,.T.);
#19586=CLOSED_SHELL('',(#19524,#19525,#19526,#19527,#19528,#19529,#19530,
#19531,#19532,#19533,#19534,#19535,#19536,#19537,#19538,#19539,#19540,#19541,
#19542,#19543,#19544,#19545,#19546,#19547,#19548,#19549,#19550,#19551,#19552,
#19553));
#22159=AXIS2_PLACEMENT_3D('',#34418,#28259,#28260);
#22160=AXIS2_PLACEMENT_3D('',#34419,#28261,#28262);
#22161=AXIS2_PLACEMENT_3D('',#34422,#28263,#28264);
#22162=AXIS2_PLACEMENT_3D('',#34425,#28266,#28267);
#22163=AXIS2_PLACEMENT_3D('',#34426,#28268,#28269);
#22164=AXIS2_PLACEMENT_3D('',#34427,#28270,#28271);
#22165=AXIS2_PLACEMENT_3D('',#34430,#28273,#28274);
#22166=AXIS2_PLACEMENT_3D('',#34431,#28275,#28276);
#22167=AXIS2_PLACEMENT_3D('',#34432,#28277,#28278);
#22168=AXIS2_PLACEMENT_3D('',#34446,#28279,#28280);
#22169=AXIS2_PLACEMENT_3D('',#34458,#28281,#28282);
#22170=AXIS2_PLACEMENT_3D('',#34459,#28283,#28284);
#22171=AXIS2_PLACEMENT_3D('',#34465,#28285,#28286);
#22172=AXIS2_PLACEMENT_3D('',#34469,#28287,#28288);
#22173=AXIS2_PLACEMENT_3D('',#34483,#28289,#28290);
#22174=AXIS2_PLACEMENT_3D('',#34495,#28291,#28292);
#22175=AXIS2_PLACEMENT_3D('',#34496,#28293,#28294);
#22176=AXIS2_PLACEMENT_3D('',#34502,#28295,#28296);
#22177=AXIS2_PLACEMENT_3D('',#34506,#28297,#28298);
#22178=AXIS2_PLACEMENT_3D('',#34520,#28299,#28300);
#22179=AXIS2_PLACEMENT_3D('',#34532,#28301,#28302);
#22180=AXIS2_PLACEMENT_3D('',#34533,#28303,#28304);
#22181=AXIS2_PLACEMENT_3D('',#34539,#28305,#28306);
#22182=AXIS2_PLACEMENT_3D('',#34541,#28307,#28308);
#22183=AXIS2_PLACEMENT_3D('',#34545,#28309,#28310);
#22184=AXIS2_PLACEMENT_3D('',#34559,#28311,#28312);
#22185=AXIS2_PLACEMENT_3D('',#34571,#28313,#28314);
#22186=AXIS2_PLACEMENT_3D('',#34572,#28315,#28316);
#22187=AXIS2_PLACEMENT_3D('',#34578,#28317,#28318);
#22188=AXIS2_PLACEMENT_3D('',#34582,#28319,#28320);
#22189=AXIS2_PLACEMENT_3D('',#34585,#28321,#28322);
#22190=AXIS2_PLACEMENT_3D('',#34587,#28323,#28324);
#22191=AXIS2_PLACEMENT_3D('',#34588,#28325,#28326);
#22192=AXIS2_PLACEMENT_3D('',#34589,#28327,#28328);
#22193=AXIS2_PLACEMENT_3D('',#34590,#28329,#28330);
#22194=AXIS2_PLACEMENT_3D('',#34592,#28331,#28332);
#22195=AXIS2_PLACEMENT_3D('',#34604,#28333,#28334);
#22196=AXIS2_PLACEMENT_3D('',#34606,#28335,#28336);
#22197=AXIS2_PLACEMENT_3D('',#34618,#28337,#28338);
#22198=AXIS2_PLACEMENT_3D('',#34620,#28339,#28340);
#22199=AXIS2_PLACEMENT_3D('',#34632,#28341,#28342);
#22200=AXIS2_PLACEMENT_3D('',#34634,#28343,#28344);
#22201=AXIS2_PLACEMENT_3D('',#34646,#28345,#28346);
#22202=AXIS2_PLACEMENT_3D('',#34647,#28347,#28348);
#22203=AXIS2_PLACEMENT_3D('',#34649,#28349,#28350);
#22204=AXIS2_PLACEMENT_3D('',#34651,#28352,#28353);
#22205=AXIS2_PLACEMENT_3D('',#34670,#28356,#28357);
#22206=AXIS2_PLACEMENT_3D('',#34674,#28358,#28359);
#22207=AXIS2_PLACEMENT_3D('',#34680,#28361,#28362);
#22208=AXIS2_PLACEMENT_3D('',#34697,#28364,#28365);
#22209=AXIS2_PLACEMENT_3D('',#34703,#28367,#28368);
#22210=AXIS2_PLACEMENT_3D('',#34707,#28369,#28370);
#22211=AXIS2_PLACEMENT_3D('',#34711,#28371,#28372);
#22212=AXIS2_PLACEMENT_3D('',#34717,#28374,#28375);
#22213=AXIS2_PLACEMENT_3D('',#34723,#28377,#28378);
#22214=AXIS2_PLACEMENT_3D('',#34738,#28379,#28380);
#22215=AXIS2_PLACEMENT_3D('',#34755,#28382,#28383);
#22216=AXIS2_PLACEMENT_3D('',#34759,#28384,#28385);
#22217=AXIS2_PLACEMENT_3D('',#34762,#28387,#28388);
#22218=AXIS2_PLACEMENT_3D('',#34764,#28389,#28390);
#22219=AXIS2_PLACEMENT_3D('',#34767,#28392,#28393);
#22220=AXIS2_PLACEMENT_3D('',#34768,#28394,#28395);
#22221=AXIS2_PLACEMENT_3D('',#34769,#28396,#28397);
#28259=DIRECTION('axis',(0.,0.,1.));
#28260=DIRECTION('refdir',(1.,0.,0.));
#28261=DIRECTION('center_axis',(6.02124417213197E-17,-1.,3.1081360155032E-32));
#28262=DIRECTION('ref_axis',(1.,6.02124417213197E-17,1.69633130794335E-33));
#28263=DIRECTION('center_axis',(-6.02124417213197E-17,1.,-3.1081360155032E-32));
#28264=DIRECTION('ref_axis',(1.,6.02124417213197E-17,1.69633130794335E-33));
#28265=DIRECTION('',(0.70699152335979,0.707222020229435,8.65814906106877E-17));
#28266=DIRECTION('center_axis',(-8.38023770707909E-12,-1.,3.10813601550178E-32));
#28267=DIRECTION('ref_axis',(1.,-8.38023770707909E-12,1.69633130820382E-33));
#28268=DIRECTION('center_axis',(-6.02124417213197E-17,1.,-3.1081360155032E-32));
#28269=DIRECTION('ref_axis',(1.,6.02124417213197E-17,1.69633130794335E-33));
#28270=DIRECTION('center_axis',(-6.02124417213197E-17,1.,-3.1081360155032E-32));
#28271=DIRECTION('ref_axis',(-1.,-6.02124417213197E-17,-1.69633130794335E-33));
#28272=DIRECTION('',(6.02124417213197E-17,-1.,3.1081360155032E-32));
#28273=DIRECTION('center_axis',(-6.02124417213197E-17,1.,-3.1081360155032E-32));
#28274=DIRECTION('ref_axis',(-1.,-6.02124417213197E-17,-1.69633130794335E-33));
#28275=DIRECTION('center_axis',(-6.02124417213197E-17,1.,-3.1081360155032E-32));
#28276=DIRECTION('ref_axis',(-1.69633130794335E-33,3.1081360155032E-32,
1.));
#28277=DIRECTION('center_axis',(-6.02124417213197E-17,1.,-3.1081360155032E-32));
#28278=DIRECTION('ref_axis',(0.,0.,-1.));
#28279=DIRECTION('center_axis',(-6.02124417213197E-17,1.,-3.1081360155032E-32));
#28280=DIRECTION('ref_axis',(-1.,-6.02124417213197E-17,7.31030425583873E-12));
#28281=DIRECTION('center_axis',(6.02123954565766E-17,-1.,-6.80180522852632E-12));
#28282=DIRECTION('ref_axis',(-1.,-6.02124417213198E-17,6.80183298410194E-12));
#28283=DIRECTION('center_axis',(6.02124417213197E-17,-1.,3.1081360155032E-32));
#28284=DIRECTION('ref_axis',(-1.,-6.02124417213197E-17,-1.69633130794335E-33));
#28285=DIRECTION('center_axis',(-6.02124417213197E-17,1.,-3.1081360155032E-32));
#28286=DIRECTION('ref_axis',(-1.,-6.02124417213197E-17,-1.69633130794335E-33));
#28287=DIRECTION('center_axis',(-6.02124417213197E-17,1.,-3.1081360155032E-32));
#28288=DIRECTION('ref_axis',(0.,0.,-1.));
#28289=DIRECTION('center_axis',(-6.02124417213197E-17,1.,-3.1081360155032E-32));
#28290=DIRECTION('ref_axis',(-7.31034016801343E-12,-4.40204512689686E-28,
-1.));
#28291=DIRECTION('center_axis',(-6.8017450160846E-12,-1.,4.62649708883395E-23));
#28292=DIRECTION('ref_axis',(-6.80186646086628E-12,-4.09588069284889E-28,
-1.));
#28293=DIRECTION('center_axis',(6.02124417213197E-17,-1.,3.1081360155032E-32));
#28294=DIRECTION('ref_axis',(-1.,-6.02124417213197E-17,-1.69633130794335E-33));
#28295=DIRECTION('center_axis',(-6.02124417213197E-17,1.,-3.1081360155032E-32));
#28296=DIRECTION('ref_axis',(-1.,-6.02124417213197E-17,-1.69633130794335E-33));
#28297=DIRECTION('center_axis',(-6.02124417213197E-17,1.,-3.1081360155032E-32));
#28298=DIRECTION('ref_axis',(0.,0.,-1.));
#28299=DIRECTION('center_axis',(-6.02124417213197E-17,1.,-3.1081360155032E-32));
#28300=DIRECTION('ref_axis',(1.,6.02124417213197E-17,1.69633130794335E-33));
#28301=DIRECTION('center_axis',(6.02123954559324E-17,-1.,6.80180522852632E-12));
#28302=DIRECTION('ref_axis',(1.,6.02124417213198E-17,6.80192769320624E-12));
#28303=DIRECTION('center_axis',(6.02124417213197E-17,-1.,3.1081360155032E-32));
#28304=DIRECTION('ref_axis',(1.,6.02124417213197E-17,1.22464679914735E-16));
#28305=DIRECTION('center_axis',(-6.02124417213197E-17,1.,-3.1081360155032E-32));
#28306=DIRECTION('ref_axis',(-1.,-6.02124417213197E-17,-1.69633130794335E-33));
#28307=DIRECTION('center_axis',(-6.02124417213197E-17,1.,-3.1081360155032E-32));
#28308=DIRECTION('ref_axis',(-1.,-6.02124417213197E-17,-1.69633130794335E-33));
#28309=DIRECTION('center_axis',(-6.02124417213197E-17,1.,-3.1081360155032E-32));
#28310=DIRECTION('ref_axis',(0.,0.,1.));
#28311=DIRECTION('center_axis',(-6.02124417213197E-17,1.,-3.1081360155032E-32));
#28312=DIRECTION('ref_axis',(-7.31034016801343E-12,-4.40142349969376E-28,
1.));
#28313=DIRECTION('center_axis',(-6.8017450160846E-12,-1.,-4.62649708261767E-23));
#28314=DIRECTION('ref_axis',(-6.80186646086628E-12,-4.09525906487E-28,1.));
#28315=DIRECTION('center_axis',(6.02124417213197E-17,-1.,3.1081360155032E-32));
#28316=DIRECTION('ref_axis',(-1.,-6.02124417213197E-17,-1.69633130794335E-33));
#28317=DIRECTION('center_axis',(-6.02124417213197E-17,1.,-3.1081360155032E-32));
#28318=DIRECTION('ref_axis',(-1.,-6.02124417213197E-17,-1.69633130794335E-33));
#28319=DIRECTION('center_axis',(-6.02124417213197E-17,1.,-3.1081360155032E-32));
#28320=DIRECTION('ref_axis',(0.,0.,-1.));
#28321=DIRECTION('center_axis',(6.02124417213197E-17,-1.,3.1081360155032E-32));
#28322=DIRECTION('ref_axis',(1.,6.02124417213197E-17,1.69633130794335E-33));
#28323=DIRECTION('center_axis',(1.,6.02124417213197E-17,0.));
#28324=DIRECTION('ref_axis',(0.,0.,1.));
#28325=DIRECTION('center_axis',(-6.02124211725949E-17,1.,-4.53300889872937E-12));
#28326=DIRECTION('ref_axis',(1.,6.02124417213197E-17,4.53313136340929E-12));
#28327=DIRECTION('center_axis',(6.02124417213197E-17,-1.,3.1081360155032E-32));
#28328=DIRECTION('ref_axis',(1.,6.02124417213197E-17,1.69633130794335E-33));
#28329=DIRECTION('center_axis',(0.,0.,1.));
#28330=DIRECTION('ref_axis',(0.0108223376335956,-0.999941436789247,0.));
#28331=DIRECTION('center_axis',(0.0407206959932429,-0.0871557427495498,
-0.995362095633343));
#28332=DIRECTION('ref_axis',(0.999164217135634,6.02779468193653E-17,0.0408762424365959));
#28333=DIRECTION('center_axis',(0.995362095633343,-0.0871557427495499,-0.0407206959932438));
#28334=DIRECTION('ref_axis',(0.0408762424365968,9.94030957902627E-18,0.999164217135634));
#28335=DIRECTION('center_axis',(-0.995362095633343,-0.08715574274955,-0.0407206959932438));
#28336=DIRECTION('ref_axis',(0.0408762424365968,-4.74217326228398E-18,-0.999164217135634));
#28337=DIRECTION('center_axis',(-0.0407206959932429,-0.0871557427495498,
-0.995362095633343));
#28338=DIRECTION('ref_axis',(0.999164217135634,5.8550611285046E-17,-0.0408762424365959));
#28339=DIRECTION('center_axis',(-0.0407206959932429,-0.0871557427495498,
0.995362095633343));
#28340=DIRECTION('ref_axis',(-0.999164217135634,-5.8550611285046E-17,-0.0408762424365959));
#28341=DIRECTION('center_axis',(-0.995362095633343,-0.08715574274955,0.0407206959932438));
#28342=DIRECTION('ref_axis',(-0.0408762424365968,4.74217326228398E-18,-0.999164217135634));
#28343=DIRECTION('center_axis',(0.995362095633343,-0.0871557427495499,0.0407206959932438));
#28344=DIRECTION('ref_axis',(-0.0408762424365968,-9.94030957902627E-18,
0.999164217135634));
#28345=DIRECTION('center_axis',(0.0407206959932429,-0.0871557427495498,
0.995362095633343));
#28346=DIRECTION('ref_axis',(-0.999164217135634,-6.02779468193653E-17,0.0408762424365959));
#28347=DIRECTION('center_axis',(-6.02124417213197E-17,1.,-3.1081360155032E-32));
#28348=DIRECTION('ref_axis',(-1.,-6.02124417213197E-17,-1.69633130794335E-33));
#28349=DIRECTION('center_axis',(-6.02124417213197E-17,1.,-3.1081360155032E-32));
#28350=DIRECTION('ref_axis',(-1.,-6.02124417213197E-17,-1.69633130794335E-33));
#28351=DIRECTION('',(-0.0348994967025007,-0.999390827019096,4.27395569285715E-18));
#28352=DIRECTION('center_axis',(-6.02124417213197E-17,1.,-3.1081360155032E-32));
#28353=DIRECTION('ref_axis',(0.999164217135713,6.01621171943121E-17,-0.0408762424346739));
#28354=DIRECTION('',(0.0035625992711232,0.996194698091663,-0.0870828994722507));
#28355=DIRECTION('',(0.0870828994722507,0.996194698091663,-0.00356259927112407));
#28356=DIRECTION('center_axis',(0.0407206959913409,-0.0871557427476582,
-0.995362095633586));
#28357=DIRECTION('ref_axis',(5.77166398093136E-17,-0.99618836566326,0.0872280924769298));
#28358=DIRECTION('center_axis',(0.0407206959913409,-0.0871557427476582,
0.995362095633586));
#28359=DIRECTION('ref_axis',(-0.905991774445375,-0.423295292481881,5.86723486602494E-17));
#28360=DIRECTION('',(0.00356259927112393,0.996194698091663,0.0870828994722507));
#28361=DIRECTION('center_axis',(-6.02124417213197E-17,1.,-3.1081360155032E-32));
#28362=DIRECTION('ref_axis',(0.0408762424346715,2.46125836538422E-18,0.999164217135713));
#28363=DIRECTION('',(0.0870828994722507,0.996194698091663,0.00356259927112347));
#28364=DIRECTION('center_axis',(-0.0407206959913409,-0.0871557427476582,
0.995362095633586));
#28365=DIRECTION('ref_axis',(-0.905991774445375,0.423295292481881,-5.86723486602494E-17));
#28366=DIRECTION('',(-0.00356259927112332,0.996194698091663,0.0870828994722507));
#28367=DIRECTION('center_axis',(0.995362095633586,-0.0871557427476581,0.0407206959913419));
#28368=DIRECTION('ref_axis',(-0.0872280924769297,-0.99618836566326,-2.68621612590795E-18));
#28369=DIRECTION('center_axis',(0.995362095633586,-0.0871557427476581,-0.0407206959913419));
#28370=DIRECTION('ref_axis',(-0.0872280924769297,-0.99618836566326,2.68621612590795E-18));
#28371=DIRECTION('center_axis',(-0.995362095633586,-0.0871557427476583,
-0.0407206959913419));
#28372=DIRECTION('ref_axis',(3.56814972436615E-17,-0.42329529248189,0.905991774445371));
#28373=DIRECTION('',(-0.0870828994722508,0.996194698091663,-0.00356259927112347));
#28374=DIRECTION('center_axis',(-0.995362095633586,-0.0871557427476583,
0.0407206959913419));
#28375=DIRECTION('ref_axis',(-3.56814972436615E-17,0.42329529248189,0.905991774445371));
#28376=DIRECTION('',(-0.0870828994722508,0.996194698091663,0.00356259927112407));
#28377=DIRECTION('center_axis',(-6.02124417213197E-17,1.,-3.1081360155032E-32));
#28378=DIRECTION('ref_axis',(-0.999164217135713,-6.01621171943121E-17,0.0408762424346739));
#28379=DIRECTION('center_axis',(-6.02124417213197E-17,1.,-3.1081360155032E-32));
#28380=DIRECTION('ref_axis',(-0.0408762424346715,-2.46125836538422E-18,
-0.999164217135713));
#28381=DIRECTION('',(-0.00356259927112405,0.996194698091663,-0.0870828994722507));
#28382=DIRECTION('center_axis',(-0.0407206959913409,-0.0871557427476582,
-0.995362095633586));
#28383=DIRECTION('ref_axis',(6.27251844107897E-17,-0.99618836566326,0.0872280924769298));
#28384=DIRECTION('center_axis',(6.02124417213197E-17,-1.,3.1081360155032E-32));
#28385=DIRECTION('ref_axis',(-1.,-6.02124417213197E-17,-1.69633130794335E-33));
#28386=DIRECTION('',(0.88294759285893,-0.469471562785886,1.08129894340955E-16));
#28387=DIRECTION('center_axis',(-6.02124417213197E-17,1.,-3.1081360155032E-32));
#28388=DIRECTION('ref_axis',(-1.,-6.02124417213197E-17,-1.69633130794335E-33));
#28389=DIRECTION('center_axis',(-6.02124417213197E-17,1.,-3.1081360155032E-32));
#28390=DIRECTION('ref_axis',(-1.,-6.02124417213197E-17,-1.69633130794335E-33));
#28391=DIRECTION('',(6.02124417213197E-17,-1.,3.1081360155032E-32));
#28392=DIRECTION('center_axis',(-6.02124417213197E-17,1.,-3.1081360155032E-32));
#28393=DIRECTION('ref_axis',(-1.,-6.02124417213197E-17,-1.69633130794335E-33));
#28394=DIRECTION('center_axis',(-6.02124417213197E-17,1.,-3.1081360155032E-32));
#28395=DIRECTION('ref_axis',(-1.69633130794335E-33,3.1081360155032E-32,
1.));
#28396=DIRECTION('center_axis',(-6.02124417213197E-17,1.,-3.1081360155032E-32));
#28397=DIRECTION('ref_axis',(-1.,-6.02124417213197E-17,-1.69633130794335E-33));
#28398=DIRECTION('',(-0.403628089275423,-0.914923147345104,4.94301847577109E-17));
#34418=CARTESIAN_POINT('',(0.,0.,0.));
#34419=CARTESIAN_POINT('Origin',(0.0155,-0.0056534125,0.0155));
#34420=CARTESIAN_POINT('',(0.01700000000002,-0.00580682499999,0.0155));
#34421=CARTESIAN_POINT('',(0.013999999999995,-0.005806825000005,0.0155));
#34422=CARTESIAN_POINT('Origin',(0.01550000000001,-0.00580682499999,0.0155));
#34423=CARTESIAN_POINT('',(0.01430672500001,-0.00549999999998999,0.0155));
#34424=CARTESIAN_POINT('',(0.0141533625,-0.0056534125,0.0155));
#34425=CARTESIAN_POINT('Origin',(0.01550000000001,-0.00549999999999,0.0155));
#34426=CARTESIAN_POINT('Origin',(0.01550000000001,-0.00580682499999,0.0155));
#34427=CARTESIAN_POINT('Origin',(0.0155,-0.0175,0.0155));
#34428=CARTESIAN_POINT('',(0.017,-0.02949999999999,0.0155));
#34429=CARTESIAN_POINT('',(0.017,-0.0175,0.0155));
#34430=CARTESIAN_POINT('Origin',(0.01550000000001,-0.02949999999999,0.0155));
#34431=CARTESIAN_POINT('Origin',(0.01475,-0.0055,0.0155));
#34432=CARTESIAN_POINT('Origin',(0.0155,-0.0325967679907942,0.0155));
#34433=CARTESIAN_POINT('',(0.0140430296811173,-0.0326789662095993,0.0153032273967176));
#34434=CARTESIAN_POINT('',(0.0141463367962054,-0.0326351410015245,0.0153028384738583));
#34435=CARTESIAN_POINT('Ctrl Pts',(0.0141463367962063,-0.0326351410015253,
0.015302838473864));
#34436=CARTESIAN_POINT('Ctrl Pts',(0.0141423240437266,-0.032643263445668,
0.0153022914211073));
#34437=CARTESIAN_POINT('Ctrl Pts',(0.0141364374786249,-0.032651336899898,
0.0153018253164866));
#34438=CARTESIAN_POINT('Ctrl Pts',(0.0141228216222177,-0.0326649719690126,
0.0153011884352657));
#34439=CARTESIAN_POINT('Ctrl Pts',(0.0141121610166096,-0.032672062422094,
0.0153010037121127));
#34440=CARTESIAN_POINT('Ctrl Pts',(0.0140922949035023,-0.0326802644698773,
0.0153010982569886));
#34441=CARTESIAN_POINT('Ctrl Pts',(0.0140795551609431,-0.0326827679907942,
0.0153014002324808));
#34442=CARTESIAN_POINT('Ctrl Pts',(0.0140605993929865,-0.0326827679907942,
0.0153021757211875));
#34443=CARTESIAN_POINT('Ctrl Pts',(0.0140513381771173,-0.0326814761879823,
0.0153026677141935));
#34444=CARTESIAN_POINT('Ctrl Pts',(0.0140430296811173,-0.0326789662095993,
0.0153032273967175));
#34445=CARTESIAN_POINT('',(0.0141463367962067,-0.0326351410015237,0.0156971615261415));
#34446=CARTESIAN_POINT('Origin',(0.0155,-0.0326351410027316,0.01549999999999));
#34447=CARTESIAN_POINT('',(0.0140430296811173,-0.0326789662095993,0.0156967726032824));
#34448=CARTESIAN_POINT('Ctrl Pts',(0.0140430296811173,-0.0326789662095993,
0.0156967726032824));
#34449=CARTESIAN_POINT('Ctrl Pts',(0.0140513381771173,-0.0326814761879823,
0.0156973322858065));
#34450=CARTESIAN_POINT('Ctrl Pts',(0.0140605993929865,-0.0326827679907942,
0.0156978242788125));
#34451=CARTESIAN_POINT('Ctrl Pts',(0.0140795551609431,-0.0326827679907942,
0.0156985997675192));
#34452=CARTESIAN_POINT('Ctrl Pts',(0.0140922949035023,-0.0326802644698773,
0.0156989017430114));
#34453=CARTESIAN_POINT('Ctrl Pts',(0.0141121610166096,-0.032672062422094,
0.0156989962878872));
#34454=CARTESIAN_POINT('Ctrl Pts',(0.0141228216222177,-0.0326649719690126,
0.0156988115647342));
#34455=CARTESIAN_POINT('Ctrl Pts',(0.0141364374786252,-0.0326513368998977,
0.0156981746835134));
#34456=CARTESIAN_POINT('Ctrl Pts',(0.0141423240437271,-0.0326432634456672,
0.0156977085788927));
#34457=CARTESIAN_POINT('Ctrl Pts',(0.0141463367962069,-0.0326351410015241,
0.0156971615261359));
#34458=CARTESIAN_POINT('Origin',(0.01549999999999,-0.0326789662096093,0.0155));
#34459=CARTESIAN_POINT('Origin',(0.0155,-0.0321179414315921,0.0155));
#34460=CARTESIAN_POINT('',(0.0146893860964955,-0.0315359551043615,0.0153768688374301));
#34461=CARTESIAN_POINT('Ctrl Pts',(0.0141463367962063,-0.0326351410015253,
0.015302838473864));
#34462=CARTESIAN_POINT('Ctrl Pts',(0.0144860139927036,-0.0319475807897096,
0.0153491461736378));
#34463=CARTESIAN_POINT('Ctrl Pts',(0.0146893860964955,-0.0315359551043615,
0.0153768688374301));
#34464=CARTESIAN_POINT('',(0.0146893860964955,-0.0315359551043615,0.0156231311625699));
#34465=CARTESIAN_POINT('Origin',(0.01550000000001,-0.0315359551043715,0.0155));
#34466=CARTESIAN_POINT('Ctrl Pts',(0.0146893860964954,-0.0315359551043615,
0.0156231311625699));
#34467=CARTESIAN_POINT('Ctrl Pts',(0.0144860139924889,-0.0319475807901437,
0.0156508538263914));
#34468=CARTESIAN_POINT('Ctrl Pts',(0.0141463367962068,-0.0326351410015241,
0.0156971615261359));
#34469=CARTESIAN_POINT('Origin',(0.0155,-0.0325967679907942,0.0155));
#34470=CARTESIAN_POINT('',(0.0156967726032824,-0.0326789662095993,0.0140430296811173));
#34471=CARTESIAN_POINT('',(0.0156971615261417,-0.0326351410015244,0.0141463367962054));
#34472=CARTESIAN_POINT('Ctrl Pts',(0.015697161526136,-0.0326351410015253,
0.0141463367962063));
#34473=CARTESIAN_POINT('Ctrl Pts',(0.0156977085788927,-0.032643263445668,
0.0141423240437266));
#34474=CARTESIAN_POINT('Ctrl Pts',(0.0156981746835134,-0.032651336899898,
0.0141364374786249));
#34475=CARTESIAN_POINT('Ctrl Pts',(0.0156988115647343,-0.0326649719690126,
0.0141228216222177));
#34476=CARTESIAN_POINT('Ctrl Pts',(0.0156989962878873,-0.032672062422094,
0.0141121610166096));
#34477=CARTESIAN_POINT('Ctrl Pts',(0.0156989017430114,-0.0326802644698773,
0.0140922949035023));
#34478=CARTESIAN_POINT('Ctrl Pts',(0.0156985997675192,-0.0326827679907942,
0.0140795551609431));
#34479=CARTESIAN_POINT('Ctrl Pts',(0.0156978242788125,-0.0326827679907942,
0.0140605993929865));
#34480=CARTESIAN_POINT('Ctrl Pts',(0.0156973322858065,-0.0326814761879823,
0.0140513381771173));
#34481=CARTESIAN_POINT('Ctrl Pts',(0.0156967726032825,-0.0326789662095993,
0.0140430296811173));
#34482=CARTESIAN_POINT('',(0.0153028384738585,-0.0326351410015237,0.0141463367962067));
#34483=CARTESIAN_POINT('Origin',(0.01550000000001,-0.0326351410027316,0.0155));
#34484=CARTESIAN_POINT('',(0.0153032273967176,-0.0326789662095993,0.0140430296811173));
#34485=CARTESIAN_POINT('Ctrl Pts',(0.0153032273967176,-0.0326789662095993,
0.0140430296811173));
#34486=CARTESIAN_POINT('Ctrl Pts',(0.0153026677141935,-0.0326814761879823,
0.0140513381771173));
#34487=CARTESIAN_POINT('Ctrl Pts',(0.0153021757211875,-0.0326827679907942,
0.0140605993929865));
#34488=CARTESIAN_POINT('Ctrl Pts',(0.0153014002324808,-0.0326827679907942,
0.0140795551609431));
#34489=CARTESIAN_POINT('Ctrl Pts',(0.0153010982569886,-0.0326802644698773,
0.0140922949035023));
#34490=CARTESIAN_POINT('Ctrl Pts',(0.0153010037121128,-0.032672062422094,
0.0141121610166096));
#34491=CARTESIAN_POINT('Ctrl Pts',(0.0153011884352658,-0.0326649719690126,
0.0141228216222177));
#34492=CARTESIAN_POINT('Ctrl Pts',(0.0153018253164866,-0.0326513368998977,
0.0141364374786252));
#34493=CARTESIAN_POINT('Ctrl Pts',(0.0153022914211073,-0.0326432634456672,
0.0141423240437272));
#34494=CARTESIAN_POINT('Ctrl Pts',(0.0153028384738641,-0.0326351410015241,
0.0141463367962069));
#34495=CARTESIAN_POINT('Origin',(0.01549999999999,-0.0326789662096093,0.0155));
#34496=CARTESIAN_POINT('Origin',(0.0155,-0.0321179414315921,0.0155));
#34497=CARTESIAN_POINT('',(0.0156231311625699,-0.0315359551043615,0.0146893860964955));
#34498=CARTESIAN_POINT('Ctrl Pts',(0.015697161526136,-0.0326351410015253,
0.0141463367962062));
#34499=CARTESIAN_POINT('Ctrl Pts',(0.0156508538263853,-0.0319475807900528,
0.0144860139925339));
#34500=CARTESIAN_POINT('Ctrl Pts',(0.0156231311625699,-0.0315359551043615,
0.0146893860964954));
#34501=CARTESIAN_POINT('',(0.0153768688374301,-0.0315359551043615,0.0146893860964955));
#34502=CARTESIAN_POINT('Origin',(0.01550000000001,-0.0315359551043715,0.0155));
#34503=CARTESIAN_POINT('Ctrl Pts',(0.0153768688374302,-0.0315359551043615,
0.0146893860964954));
#34504=CARTESIAN_POINT('Ctrl Pts',(0.015349146173611,-0.0319475807901076,
0.0144860139925067));
#34505=CARTESIAN_POINT('Ctrl Pts',(0.0153028384738641,-0.0326351410015241,
0.0141463367962068));
#34506=CARTESIAN_POINT('Origin',(0.0155,-0.0325967679907942,0.0155));
#34507=CARTESIAN_POINT('',(0.0169569703188827,-0.0326789662095993,0.0156967726032824));
#34508=CARTESIAN_POINT('',(0.0168536632037933,-0.0326351410015237,0.0156971615261415));
#34509=CARTESIAN_POINT('Ctrl Pts',(0.0168536632037931,-0.0326351410015241,
0.0156971615261359));
#34510=CARTESIAN_POINT('Ctrl Pts',(0.0168576759562728,-0.0326432634456672,
0.0156977085788927));
#34511=CARTESIAN_POINT('Ctrl Pts',(0.0168635625213748,-0.0326513368998977,
0.0156981746835134));
#34512=CARTESIAN_POINT('Ctrl Pts',(0.0168771783777823,-0.0326649719690126,
0.0156988115647343));
#34513=CARTESIAN_POINT('Ctrl Pts',(0.0168878389833904,-0.032672062422094,
0.0156989962878873));
#34514=CARTESIAN_POINT('Ctrl Pts',(0.0169077050964977,-0.0326802644698773,
0.0156989017430114));
#34515=CARTESIAN_POINT('Ctrl Pts',(0.0169204448390569,-0.0326827679907942,
0.0156985997675192));
#34516=CARTESIAN_POINT('Ctrl Pts',(0.0169394006070135,-0.0326827679907942,
0.0156978242788125));
#34517=CARTESIAN_POINT('Ctrl Pts',(0.0169486618228827,-0.0326814761879823,
0.0156973322858065));
#34518=CARTESIAN_POINT('Ctrl Pts',(0.0169569703188827,-0.0326789662095993,
0.0156967726032825));
#34519=CARTESIAN_POINT('',(0.0168536632037947,-0.0326351410015244,0.0153028384738584));
#34520=CARTESIAN_POINT('Origin',(0.0155,-0.0326351410027316,0.01549999999999));
#34521=CARTESIAN_POINT('',(0.0169569703188827,-0.0326789662095993,0.0153032273967176));
#34522=CARTESIAN_POINT('Ctrl Pts',(0.0169569703188827,-0.0326789662095993,
0.0153032273967176));
#34523=CARTESIAN_POINT('Ctrl Pts',(0.0169486618228827,-0.0326814761879823,
0.0153026677141935));
#34524=CARTESIAN_POINT('Ctrl Pts',(0.0169394006070135,-0.0326827679907942,
0.0153021757211875));
#34525=CARTESIAN_POINT('Ctrl Pts',(0.0169204448390569,-0.0326827679907942,
0.0153014002324808));
#34526=CARTESIAN_POINT('Ctrl Pts',(0.0169077050964977,-0.0326802644698773,
0.0153010982569886));
#34527=CARTESIAN_POINT('Ctrl Pts',(0.0168878389833904,-0.032672062422094,
0.0153010037121128));
#34528=CARTESIAN_POINT('Ctrl Pts',(0.0168771783777823,-0.0326649719690126,
0.0153011884352658));
#34529=CARTESIAN_POINT('Ctrl Pts',(0.0168635625213751,-0.032651336899898,
0.0153018253164866));
#34530=CARTESIAN_POINT('Ctrl Pts',(0.0168576759562734,-0.032643263445668,
0.0153022914211073));
#34531=CARTESIAN_POINT('Ctrl Pts',(0.0168536632037937,-0.0326351410015253,
0.015302838473864));
#34532=CARTESIAN_POINT('Origin',(0.01549999999999,-0.0326789662096093,0.0155));
#34533=CARTESIAN_POINT('Origin',(0.0155,-0.0321179414315921,0.0155));
#34534=CARTESIAN_POINT('',(0.0163106139035045,-0.0315359551043615,0.0156231311625699));
#34535=CARTESIAN_POINT('Ctrl Pts',(0.0168536632037932,-0.0326351410015241,
0.0156971615261359));
#34536=CARTESIAN_POINT('Ctrl Pts',(0.0165139860074969,-0.0319475807901151,
0.0156508538263895));
#34537=CARTESIAN_POINT('Ctrl Pts',(0.0163106139035046,-0.0315359551043615,
0.0156231311625699));
#34538=CARTESIAN_POINT('',(0.0163199123024952,-0.0315359551043719,0.0155));
#34539=CARTESIAN_POINT('Origin',(0.01550000000001,-0.0315359551043715,0.0155));
#34540=CARTESIAN_POINT('',(0.0163106139035045,-0.0315359551043615,0.0153768688374301));
#34541=CARTESIAN_POINT('Origin',(0.01550000000001,-0.0315359551043715,0.0155));
#34542=CARTESIAN_POINT('Ctrl Pts',(0.0163106139035046,-0.0315359551043614,
0.0153768688374302));
#34543=CARTESIAN_POINT('Ctrl Pts',(0.0165139860075985,-0.0319475807903205,
0.0153491461735967));
#34544=CARTESIAN_POINT('Ctrl Pts',(0.0168536632037939,-0.0326351410015252,
0.0153028384738641));
#34545=CARTESIAN_POINT('Origin',(0.0155,-0.0325967679907942,0.0155));
#34546=CARTESIAN_POINT('',(0.0153032273967176,-0.0326789662095993,0.0169569703188827));
#34547=CARTESIAN_POINT('',(0.0153028384738585,-0.0326351410015237,0.0168536632037933));
#34548=CARTESIAN_POINT('Ctrl Pts',(0.0153028384738641,-0.0326351410015241,
0.0168536632037931));
#34549=CARTESIAN_POINT('Ctrl Pts',(0.0153022914211073,-0.0326432634456672,
0.0168576759562728));
#34550=CARTESIAN_POINT('Ctrl Pts',(0.0153018253164866,-0.0326513368998977,
0.0168635625213748));
#34551=CARTESIAN_POINT('Ctrl Pts',(0.0153011884352657,-0.0326649719690126,
0.0168771783777823));
#34552=CARTESIAN_POINT('Ctrl Pts',(0.0153010037121127,-0.032672062422094,
0.0168878389833904));
#34553=CARTESIAN_POINT('Ctrl Pts',(0.0153010982569886,-0.0326802644698773,
0.0169077050964977));
#34554=CARTESIAN_POINT('Ctrl Pts',(0.0153014002324808,-0.0326827679907942,
0.0169204448390569));
#34555=CARTESIAN_POINT('Ctrl Pts',(0.0153021757211875,-0.0326827679907942,
0.0169394006070135));
#34556=CARTESIAN_POINT('Ctrl Pts',(0.0153026677141935,-0.0326814761879823,
0.0169486618228827));
#34557=CARTESIAN_POINT('Ctrl Pts',(0.0153032273967175,-0.0326789662095993,
0.0169569703188827));
#34558=CARTESIAN_POINT('',(0.0156971615261417,-0.0326351410015245,0.0168536632037946));
#34559=CARTESIAN_POINT('Origin',(0.01550000000001,-0.0326351410027316,0.0155));
#34560=CARTESIAN_POINT('',(0.0156967726032824,-0.0326789662095993,0.0169569703188827));
#34561=CARTESIAN_POINT('Ctrl Pts',(0.0156967726032824,-0.0326789662095993,
0.0169569703188827));
#34562=CARTESIAN_POINT('Ctrl Pts',(0.0156973322858065,-0.0326814761879823,
0.0169486618228827));
#34563=CARTESIAN_POINT('Ctrl Pts',(0.0156978242788125,-0.0326827679907942,
0.0169394006070135));
#34564=CARTESIAN_POINT('Ctrl Pts',(0.0156985997675192,-0.0326827679907942,
0.0169204448390569));
#34565=CARTESIAN_POINT('Ctrl Pts',(0.0156989017430114,-0.0326802644698773,
0.0169077050964977));
#34566=CARTESIAN_POINT('Ctrl Pts',(0.0156989962878872,-0.032672062422094,
0.0168878389833904));
#34567=CARTESIAN_POINT('Ctrl Pts',(0.0156988115647342,-0.0326649719690126,
0.0168771783777823));
#34568=CARTESIAN_POINT('Ctrl Pts',(0.0156981746835134,-0.032651336899898,
0.0168635625213751));
#34569=CARTESIAN_POINT('Ctrl Pts',(0.0156977085788927,-0.032643263445668,
0.0168576759562734));
#34570=CARTESIAN_POINT('Ctrl Pts',(0.015697161526136,-0.0326351410015253,
0.0168536632037937));
#34571=CARTESIAN_POINT('Origin',(0.01549999999999,-0.0326789662096093,0.0155));
#34572=CARTESIAN_POINT('Origin',(0.0155,-0.0321179414315921,0.0155));
#34573=CARTESIAN_POINT('',(0.0153768688374301,-0.0315359551043615,0.0163106139035045));
#34574=CARTESIAN_POINT('Ctrl Pts',(0.0153028384738641,-0.0326351410015241,
0.0168536632037932));
#34575=CARTESIAN_POINT('Ctrl Pts',(0.0153491461736176,-0.0319475807900087,
0.0165139860074444));
#34576=CARTESIAN_POINT('Ctrl Pts',(0.0153768688374301,-0.0315359551043615,
0.0163106139035046));
#34577=CARTESIAN_POINT('',(0.0156231311625699,-0.0315359551043615,0.0163106139035045));
#34578=CARTESIAN_POINT('Origin',(0.01550000000001,-0.0315359551043715,0.0155));
#34579=CARTESIAN_POINT('Ctrl Pts',(0.0156231311625699,-0.0315359551043615,
0.0163106139035045));
#34580=CARTESIAN_POINT('Ctrl Pts',(0.0156508538263448,-0.0319475807894513,
0.0165139860071687));
#34581=CARTESIAN_POINT('Ctrl Pts',(0.015697161526136,-0.0326351410015254,
0.0168536632037936));
#34582=CARTESIAN_POINT('Origin',(0.0155,-0.0314896193890613,0.0155));
#34583=CARTESIAN_POINT('',(0.0182642230121603,-0.0315245188857739,0.01549999999999));
#34584=CARTESIAN_POINT('',(0.0155,-0.0315245188857739,0.0182642230121503));
#34585=CARTESIAN_POINT('Origin',(0.0155,-0.0315245188857739,0.01549999999999));
#34586=CARTESIAN_POINT('',(0.0155,-0.0323870242363267,0.017706040231424));
#34587=CARTESIAN_POINT('Origin',(0.0155,-0.0314896193890613,0.0172648321851312));
#34588=CARTESIAN_POINT('Origin',(0.01550000000001,-0.0323870242363367,0.0155));
#34589=CARTESIAN_POINT('Origin',(0.0155,-0.0315245188857739,0.01549999999999));
#34590=CARTESIAN_POINT('Origin',(0.0155,-0.0279,0.0155));
#34591=CARTESIAN_POINT('',(0.0150423056295014,-0.0328724938596638,0.0157545990550246));
#34592=CARTESIAN_POINT('Origin',(0.0155065692871957,-0.0279140604449322,
0.0153394226989194));
#34593=CARTESIAN_POINT('',(0.0152454009449754,-0.0328724938596638,0.0159576943704986));
#34594=CARTESIAN_POINT('Ctrl Pts',(0.0150423056295014,-0.0328724938596638,
0.0157545990550246));
#34595=CARTESIAN_POINT('Ctrl Pts',(0.0150636146923879,-0.0328744020667681,
0.0157556379041868));
#34596=CARTESIAN_POINT('Ctrl Pts',(0.0150856203042815,-0.0328760596977499,
0.0157600236941645));
#34597=CARTESIAN_POINT('Ctrl Pts',(0.0151328421380346,-0.0328788497729191,
0.0157775788158223));
#34598=CARTESIAN_POINT('Ctrl Pts',(0.0151572787782427,-0.0328797021837751,
0.0157929445962307));
#34599=CARTESIAN_POINT('Ctrl Pts',(0.0151963759161913,-0.0328799869200382,
0.0158290125584882));
#34600=CARTESIAN_POINT('Ctrl Pts',(0.0152136491665739,-0.032879439770222,
0.0158521091581119));
#34601=CARTESIAN_POINT('Ctrl Pts',(0.0152375167802226,-0.0328768773126286,
0.0159032280479782));
#34602=CARTESIAN_POINT('Ctrl Pts',(0.0152441117443853,-0.0328748619240703,
0.0159312500536082));
#34603=CARTESIAN_POINT('Ctrl Pts',(0.0152454009449754,-0.0328724938596638,
0.0159576943704985));
#34604=CARTESIAN_POINT('Origin',(0.0156605773010806,-0.0279140604449322,
0.0154934307128043));
#34605=CARTESIAN_POINT('',(0.0157545990550246,-0.0328724938596638,0.0159576943704986));
#34606=CARTESIAN_POINT('Origin',(0.0153394226989194,-0.0279140604449322,
0.0154934307128043));
#34607=CARTESIAN_POINT('',(0.0159576943704986,-0.0328724938596638,0.0157545990550246));
#34608=CARTESIAN_POINT('Ctrl Pts',(0.0157545990550246,-0.0328724938596638,
0.0159576943704986));
#34609=CARTESIAN_POINT('Ctrl Pts',(0.0157556379041868,-0.0328744020667681,
0.0159363853076121));
#34610=CARTESIAN_POINT('Ctrl Pts',(0.0157600236941645,-0.0328760596977499,
0.0159143796957185));
#34611=CARTESIAN_POINT('Ctrl Pts',(0.0157775788158223,-0.0328788497729191,
0.0158671578619654));
#34612=CARTESIAN_POINT('Ctrl Pts',(0.0157929445962307,-0.0328797021837751,
0.0158427212217573));
#34613=CARTESIAN_POINT('Ctrl Pts',(0.0158290125584882,-0.0328799869200382,
0.0158036240838087));
#34614=CARTESIAN_POINT('Ctrl Pts',(0.0158521091581119,-0.032879439770222,
0.0157863508334262));
#34615=CARTESIAN_POINT('Ctrl Pts',(0.0159032280479782,-0.0328768773126286,
0.0157624832197774));
#34616=CARTESIAN_POINT('Ctrl Pts',(0.0159312500536082,-0.0328748619240703,
0.0157558882556147));
#34617=CARTESIAN_POINT('Ctrl Pts',(0.0159576943704985,-0.0328724938596638,
0.0157545990550246));
#34618=CARTESIAN_POINT('Origin',(0.0154934307128043,-0.0279140604449322,
0.0153394226989194));
#34619=CARTESIAN_POINT('',(0.0159576943704986,-0.0328724938596638,0.0152454009449754));
#34620=CARTESIAN_POINT('Origin',(0.0154934307128043,-0.0279140604449322,
0.0156605773010806));
#34621=CARTESIAN_POINT('',(0.0157545990550246,-0.0328724938596638,0.0150423056295014));
#34622=CARTESIAN_POINT('Ctrl Pts',(0.0159576943704986,-0.0328724938596638,
0.0152454009449754));
#34623=CARTESIAN_POINT('Ctrl Pts',(0.0159363853076121,-0.0328744020667681,
0.0152443620958132));
#34624=CARTESIAN_POINT('Ctrl Pts',(0.0159143796957185,-0.0328760596977499,
0.0152399763058355));
#34625=CARTESIAN_POINT('Ctrl Pts',(0.0158671578619654,-0.0328788497729191,
0.0152224211841777));
#34626=CARTESIAN_POINT('Ctrl Pts',(0.0158427212217573,-0.0328797021837751,
0.0152070554037693));
#34627=CARTESIAN_POINT('Ctrl Pts',(0.0158036240838087,-0.0328799869200382,
0.0151709874415118));
#34628=CARTESIAN_POINT('Ctrl Pts',(0.0157863508334262,-0.032879439770222,
0.0151478908418881));
#34629=CARTESIAN_POINT('Ctrl Pts',(0.0157624832197774,-0.0328768773126286,
0.0150967719520218));
#34630=CARTESIAN_POINT('Ctrl Pts',(0.0157558882556147,-0.0328748619240703,
0.0150687499463918));
#34631=CARTESIAN_POINT('Ctrl Pts',(0.0157545990550246,-0.0328724938596638,
0.0150423056295015));
#34632=CARTESIAN_POINT('Origin',(0.0153394226989194,-0.0279140604449322,
0.0155065692871957));
#34633=CARTESIAN_POINT('',(0.0152454009449754,-0.0328724938596638,0.0150423056295014));
#34634=CARTESIAN_POINT('Origin',(0.0156605773010806,-0.0279140604449322,
0.0155065692871957));
#34635=CARTESIAN_POINT('',(0.0150423056295014,-0.0328724938596638,0.0152454009449754));
#34636=CARTESIAN_POINT('Ctrl Pts',(0.0152454009449754,-0.0328724938596638,
0.0150423056295014));
#34637=CARTESIAN_POINT('Ctrl Pts',(0.0152443620958132,-0.0328744020667681,
0.0150636146923879));
#34638=CARTESIAN_POINT('Ctrl Pts',(0.0152399763058355,-0.0328760596977499,
0.0150856203042815));
#34639=CARTESIAN_POINT('Ctrl Pts',(0.0152224211841777,-0.0328788497729191,
0.0151328421380346));
#34640=CARTESIAN_POINT('Ctrl Pts',(0.0152070554037693,-0.0328797021837751,
0.0151572787782427));
#34641=CARTESIAN_POINT('Ctrl Pts',(0.0151709874415118,-0.0328799869200382,
0.0151963759161913));
#34642=CARTESIAN_POINT('Ctrl Pts',(0.0151478908418881,-0.032879439770222,
0.0152136491665738));
#34643=CARTESIAN_POINT('Ctrl Pts',(0.0150967719520218,-0.0328768773126286,
0.0152375167802226));
#34644=CARTESIAN_POINT('Ctrl Pts',(0.0150687499463918,-0.0328748619240703,
0.0152441117443853));
#34645=CARTESIAN_POINT('Ctrl Pts',(0.0150423056295015,-0.0328724938596638,
0.0152454009449754));
#34646=CARTESIAN_POINT('Origin',(0.0155065692871957,-0.0279140604449322,
0.0156605773010806));
#34647=CARTESIAN_POINT('Origin',(0.0155,-0.0312896042064176,0.0155));
#34648=CARTESIAN_POINT('',(0.0183,-0.0304999999999993,0.0155));
#34649=CARTESIAN_POINT('Origin',(0.01550000000001,-0.0305,0.0155));
#34650=CARTESIAN_POINT('',(0.018272426413518,-0.0312896042064176,0.0155));
#34651=CARTESIAN_POINT('Origin',(0.0150336424994489,-0.0329,0.0159663575005511));
#34652=CARTESIAN_POINT('',(0.0150477540341485,-0.0313489793100506,0.0156214202049252));
#34653=CARTESIAN_POINT('',(0.0150422072618173,-0.03290000000001,0.0157570035192005));
#34654=CARTESIAN_POINT('',(0.0153785797950748,-0.0313489793100506,0.0159522459658515));
#34655=CARTESIAN_POINT('Ctrl Pts',(0.0150477540341485,-0.0313489793100505,
0.0156214202049251));
#34656=CARTESIAN_POINT('Ctrl Pts',(0.015081225181466,-0.031331772155721,
0.0156212828339097));
#34657=CARTESIAN_POINT('Ctrl Pts',(0.0151152486469788,-0.0313150763778198,
0.0156263588605475));
#34658=CARTESIAN_POINT('Ctrl Pts',(0.0151692545989321,-0.0312913221771079,
0.015642486377087));
#34659=CARTESIAN_POINT('Ctrl Pts',(0.0151943811304251,-0.0312812420230617,
0.015652929486056));
#34660=CARTESIAN_POINT('Ctrl Pts',(0.0152419157873653,-0.0312670678991654,
0.015680782378196));
#34661=CARTESIAN_POINT('Ctrl Pts',(0.0152643516916966,-0.031263124157519,
0.0156982209860465));
#34662=CARTESIAN_POINT('Ctrl Pts',(0.0153017790139535,-0.031263124157519,
0.0157356483083034));
#34663=CARTESIAN_POINT('Ctrl Pts',(0.015319217621804,-0.0312670678991654,
0.0157580842126347));
#34664=CARTESIAN_POINT('Ctrl Pts',(0.015347070513944,-0.0312812420230617,
0.0158056188695749));
#34665=CARTESIAN_POINT('Ctrl Pts',(0.015357513622913,-0.0312913221771079,
0.0158307454010679));
#34666=CARTESIAN_POINT('Ctrl Pts',(0.0153736411394525,-0.0313150763778198,
0.0158847513530212));
#34667=CARTESIAN_POINT('Ctrl Pts',(0.0153787171660903,-0.031331772155721,
0.015918774818534));
#34668=CARTESIAN_POINT('Ctrl Pts',(0.0153785797950749,-0.0313489793100505,
0.0159522459658515));
#34669=CARTESIAN_POINT('',(0.0152429964807995,-0.03290000000001,0.0159577927381827));
#34670=CARTESIAN_POINT('Origin',(0.0140154882957686,-0.0329,0.015715));
#34671=CARTESIAN_POINT('Ctrl Pts',(0.0150477540341385,-0.0313489793100606,
0.0156214202049351));
#34672=CARTESIAN_POINT('Ctrl Pts',(0.0149179093434978,-0.031415731059247,
0.0156219531085977));
#34673=CARTESIAN_POINT('Ctrl Pts',(0.0146893860964855,-0.0315359551043715,
0.0156231311625798));
#34674=CARTESIAN_POINT('Origin',(0.0150422072618273,-0.0329,0.0152429964808095));
#34675=CARTESIAN_POINT('',(0.0150477540341485,-0.0313489793100506,0.0153785797950748));
#34676=CARTESIAN_POINT('',(0.0150422072618173,-0.03290000000001,0.0152429964807995));
#34677=CARTESIAN_POINT('Ctrl Pts',(0.0146893860964855,-0.0315359551043715,
0.0153768688374201));
#34678=CARTESIAN_POINT('Ctrl Pts',(0.0149179093434978,-0.031415731059247,
0.0153780468914023));
#34679=CARTESIAN_POINT('Ctrl Pts',(0.0150477540341385,-0.0313489793100605,
0.0153785797950649));
#34680=CARTESIAN_POINT('Origin',(0.0150336424994489,-0.0329,0.0150336424994489));
#34681=CARTESIAN_POINT('',(0.0153785797950748,-0.0313489793100506,0.0150477540341485));
#34682=CARTESIAN_POINT('',(0.0152429964807995,-0.03290000000001,0.0150422072618173));
#34683=CARTESIAN_POINT('Ctrl Pts',(0.0153785797950749,-0.0313489793100505,
0.0150477540341485));
#34684=CARTESIAN_POINT('Ctrl Pts',(0.0153787171660903,-0.031331772155721,
0.015081225181466));
#34685=CARTESIAN_POINT('Ctrl Pts',(0.0153736411394525,-0.0313150763778198,
0.0151152486469788));
#34686=CARTESIAN_POINT('Ctrl Pts',(0.015357513622913,-0.0312913221771079,
0.0151692545989321));
#34687=CARTESIAN_POINT('Ctrl Pts',(0.015347070513944,-0.0312812420230617,
0.0151943811304251));
#34688=CARTESIAN_POINT('Ctrl Pts',(0.015319217621804,-0.0312670678991654,
0.0152419157873653));
#34689=CARTESIAN_POINT('Ctrl Pts',(0.0153017790139535,-0.031263124157519,
0.0152643516916966));
#34690=CARTESIAN_POINT('Ctrl Pts',(0.0152643516916966,-0.031263124157519,
0.0153017790139535));
#34691=CARTESIAN_POINT('Ctrl Pts',(0.0152419157873653,-0.0312670678991654,
0.015319217621804));
#34692=CARTESIAN_POINT('Ctrl Pts',(0.0151943811304251,-0.0312812420230617,
0.015347070513944));
#34693=CARTESIAN_POINT('Ctrl Pts',(0.0151692545989321,-0.0312913221771079,
0.015357513622913));
#34694=CARTESIAN_POINT('Ctrl Pts',(0.0151152486469788,-0.0313150763778198,
0.0153736411394525));
#34695=CARTESIAN_POINT('Ctrl Pts',(0.015081225181466,-0.031331772155721,
0.0153787171660903));
#34696=CARTESIAN_POINT('Ctrl Pts',(0.0150477540341485,-0.0313489793100505,
0.0153785797950749));
#34697=CARTESIAN_POINT('Origin',(0.0169845117042314,-0.0329,0.015285));
#34698=CARTESIAN_POINT('',(0.0159522459658515,-0.0313489793100506,0.0153785797950748));
#34699=CARTESIAN_POINT('Ctrl Pts',(0.0159522459658615,-0.0313489793100606,
0.0153785797950649));
#34700=CARTESIAN_POINT('Ctrl Pts',(0.0160820906565023,-0.031415731059247,
0.0153780468914023));
#34701=CARTESIAN_POINT('Ctrl Pts',(0.0163106139035145,-0.0315359551043715,
0.0153768688374201));
#34702=CARTESIAN_POINT('',(0.0159577927381827,-0.03290000000001,0.0152429964807995));
#34703=CARTESIAN_POINT('Origin',(0.015285,-0.0329,0.0140154882957686));
#34704=CARTESIAN_POINT('Ctrl Pts',(0.0153785797950649,-0.0313489793100605,
0.0150477540341385));
#34705=CARTESIAN_POINT('Ctrl Pts',(0.0153780468914023,-0.031415731059247,
0.0149179093434977));
#34706=CARTESIAN_POINT('Ctrl Pts',(0.0153768688374201,-0.0315359551043715,
0.0146893860964855));
#34707=CARTESIAN_POINT('Origin',(0.0152429964808095,-0.0329,0.0159577927381728));
#34708=CARTESIAN_POINT('Ctrl Pts',(0.0153768688374201,-0.0315359551043715,
0.0163106139035145));
#34709=CARTESIAN_POINT('Ctrl Pts',(0.0153780468914023,-0.031415731059247,
0.0160820906565023));
#34710=CARTESIAN_POINT('Ctrl Pts',(0.0153785797950649,-0.0313489793100605,
0.0159522459658615));
#34711=CARTESIAN_POINT('Origin',(0.015715,-0.0329,0.0169845117042314));
#34712=CARTESIAN_POINT('',(0.0156214202049252,-0.0313489793100506,0.0159522459658515));
#34713=CARTESIAN_POINT('Ctrl Pts',(0.0156214202049351,-0.0313489793100605,
0.0159522459658615));
#34714=CARTESIAN_POINT('Ctrl Pts',(0.0156219531085977,-0.031415731059247,
0.0160820906565023));
#34715=CARTESIAN_POINT('Ctrl Pts',(0.0156231311625798,-0.0315359551043715,
0.0163106139035145));
#34716=CARTESIAN_POINT('',(0.0157570035192005,-0.03290000000001,0.0159577927381827));
#34717=CARTESIAN_POINT('Origin',(0.0157570035191905,-0.0329,0.0150422072618273));
#34718=CARTESIAN_POINT('',(0.0156214202049252,-0.0313489793100506,0.0150477540341485));
#34719=CARTESIAN_POINT('',(0.0157570035192005,-0.03290000000001,0.0150422072618173));
#34720=CARTESIAN_POINT('Ctrl Pts',(0.0156231311625798,-0.0315359551043715,
0.0146893860964855));
#34721=CARTESIAN_POINT('Ctrl Pts',(0.0156219531085977,-0.031415731059247,
0.0149179093434978));
#34722=CARTESIAN_POINT('Ctrl Pts',(0.0156214202049351,-0.0313489793100605,
0.0150477540341385));
#34723=CARTESIAN_POINT('Origin',(0.0159663575005511,-0.0329,0.0150336424994489));
#34724=CARTESIAN_POINT('Ctrl Pts',(0.0159522459658515,-0.0313489793100505,
0.0153785797950749));
#34725=CARTESIAN_POINT('Ctrl Pts',(0.015918774818534,-0.031331772155721,
0.0153787171660903));
#34726=CARTESIAN_POINT('Ctrl Pts',(0.0158847513530212,-0.0313150763778198,
0.0153736411394525));
#34727=CARTESIAN_POINT('Ctrl Pts',(0.0158307454010679,-0.0312913221771079,
0.015357513622913));
#34728=CARTESIAN_POINT('Ctrl Pts',(0.0158056188695749,-0.0312812420230617,
0.015347070513944));
#34729=CARTESIAN_POINT('Ctrl Pts',(0.0157580842126347,-0.0312670678991654,
0.015319217621804));
#34730=CARTESIAN_POINT('Ctrl Pts',(0.0157356483083034,-0.031263124157519,
0.0153017790139535));
#34731=CARTESIAN_POINT('Ctrl Pts',(0.0156982209860465,-0.031263124157519,
0.0152643516916966));
#34732=CARTESIAN_POINT('Ctrl Pts',(0.015680782378196,-0.0312670678991654,
0.0152419157873653));
#34733=CARTESIAN_POINT('Ctrl Pts',(0.015652929486056,-0.0312812420230617,
0.0151943811304251));
#34734=CARTESIAN_POINT('Ctrl Pts',(0.015642486377087,-0.0312913221771079,
0.0151692545989321));
#34735=CARTESIAN_POINT('Ctrl Pts',(0.0156263588605475,-0.0313150763778198,
0.0151152486469788));
#34736=CARTESIAN_POINT('Ctrl Pts',(0.0156212828339097,-0.031331772155721,
0.015081225181466));
#34737=CARTESIAN_POINT('Ctrl Pts',(0.0156214202049251,-0.0313489793100505,
0.0150477540341485));
#34738=CARTESIAN_POINT('Origin',(0.0159663575005511,-0.0329,0.0159663575005511));
#34739=CARTESIAN_POINT('',(0.0159522459658515,-0.0313489793100506,0.0156214202049252));
#34740=CARTESIAN_POINT('Ctrl Pts',(0.0156214202049251,-0.0313489793100505,
0.0159522459658515));
#34741=CARTESIAN_POINT('Ctrl Pts',(0.0156212828339097,-0.031331772155721,
0.015918774818534));
#34742=CARTESIAN_POINT('Ctrl Pts',(0.0156263588605475,-0.0313150763778198,
0.0158847513530212));
#34743=CARTESIAN_POINT('Ctrl Pts',(0.015642486377087,-0.0312913221771079,
0.0158307454010679));
#34744=CARTESIAN_POINT('Ctrl Pts',(0.015652929486056,-0.0312812420230617,
0.0158056188695749));
#34745=CARTESIAN_POINT('Ctrl Pts',(0.015680782378196,-0.0312670678991654,
0.0157580842126347));
#34746=CARTESIAN_POINT('Ctrl Pts',(0.0156982209860465,-0.031263124157519,
0.0157356483083034));
#34747=CARTESIAN_POINT('Ctrl Pts',(0.0157356483083034,-0.031263124157519,
0.0156982209860465));
#34748=CARTESIAN_POINT('Ctrl Pts',(0.0157580842126347,-0.0312670678991654,
0.015680782378196));
#34749=CARTESIAN_POINT('Ctrl Pts',(0.0158056188695749,-0.0312812420230617,
0.015652929486056));
#34750=CARTESIAN_POINT('Ctrl Pts',(0.0158307454010679,-0.0312913221771079,
0.015642486377087));
#34751=CARTESIAN_POINT('Ctrl Pts',(0.0158847513530212,-0.0313150763778198,
0.0156263588605475));
#34752=CARTESIAN_POINT('Ctrl Pts',(0.015918774818534,-0.031331772155721,
0.0156212828339097));
#34753=CARTESIAN_POINT('Ctrl Pts',(0.0159522459658515,-0.0313489793100505,
0.0156214202049251));
#34754=CARTESIAN_POINT('',(0.0159577927381827,-0.03290000000001,0.0157570035192005));
#34755=CARTESIAN_POINT('Origin',(0.0159577927381728,-0.0329,0.0157570035191905));
#34756=CARTESIAN_POINT('Ctrl Pts',(0.0163106139035145,-0.0315359551043715,
0.0156231311625798));
#34757=CARTESIAN_POINT('Ctrl Pts',(0.0160820906565023,-0.031415731059247,
0.0156219531085977));
#34758=CARTESIAN_POINT('Ctrl Pts',(0.0159522459658615,-0.0313489793100605,
0.0156214202049351));
#34759=CARTESIAN_POINT('Origin',(0.0155,-0.0313179775521807,0.0155));
#34760=CARTESIAN_POINT('',(0.0155,-0.0311,0.0155));
#34761=CARTESIAN_POINT('',(0.0159099561512377,-0.0313179775521807,0.0155));
#34762=CARTESIAN_POINT('Origin',(0.0155,-0.0301533625,0.0155));
#34763=CARTESIAN_POINT('',(0.016864685,-0.02980672499999,0.0155));
#34764=CARTESIAN_POINT('Origin',(0.01550000000001,-0.02980672499999,0.0155));
#34765=CARTESIAN_POINT('',(0.016864685,-0.0305,0.0155));
#34766=CARTESIAN_POINT('',(0.016864685,-0.0301533625,0.0155));
#34767=CARTESIAN_POINT('Origin',(0.01550000000001,-0.0305,0.0155));
#34768=CARTESIAN_POINT('Origin',(0.0134176575,-0.0305,0.0155));
#34769=CARTESIAN_POINT('Origin',(0.0155,-0.0296533625,0.0155));
#34770=CARTESIAN_POINT('',(0.0169323425,-0.0296533625,0.0155));
#34840=UNCERTAINTY_MEASURE_WITH_UNIT(LENGTH_MEASURE(1.E-5),#34877,
'DISTANCE_ACCURACY_VALUE',
'Maximum model space distance between geometric entities at asserted c
onnectivities');
#34841=UNCERTAINTY_MEASURE_WITH_UNIT(LENGTH_MEASURE(1.E-5),#34877,
'DISTANCE_ACCURACY_VALUE',
'Maximum model space distance between geometric entities at asserted c
onnectivities');
#34875=(
GEOMETRIC_REPRESENTATION_CONTEXT(3)
GLOBAL_UNCERTAINTY_ASSIGNED_CONTEXT((#34840))
GLOBAL_UNIT_ASSIGNED_CONTEXT((#34877,#34878,#34879))
REPRESENTATION_CONTEXT('','3D')
);
#34876=(
GEOMETRIC_REPRESENTATION_CONTEXT(3)
GLOBAL_UNCERTAINTY_ASSIGNED_CONTEXT((#34841))
GLOBAL_UNIT_ASSIGNED_CONTEXT((#34877,#34878,#34879))
REPRESENTATION_CONTEXT('','3D')
);
#34877=(
LENGTH_UNIT()
NAMED_UNIT(*)
SI_UNIT($,.METRE.)
);
#34878=(
NAMED_UNIT(*)
PLANE_ANGLE_UNIT()
SI_UNIT($,.RADIAN.)
);
#34879=(
NAMED_UNIT(*)
SI_UNIT($,.STERADIAN.)
SOLID_ANGLE_UNIT()
);
#34913=SHAPE_DEFINITION_REPRESENTATION(#34947,#35017);
#34947=PRODUCT_DEFINITION_SHAPE('',$,#35052);
#35017=SHAPE_REPRESENTATION('',(#22159),#34875);
#35018=PRODUCT_DEFINITION_CONTEXT('part definition',#35122,'design');
#35052=PRODUCT_DEFINITION('Pan Head Screw M3x25 1',
'Pan Head Screw M3x25 1',#35086,#35018);
#35086=PRODUCT_DEFINITION_FORMATION('',$,#35157);
#35122=APPLICATION_CONTEXT('Managed model based 3d engineering');
#35123=PRODUCT_CONTEXT('part definition',#35122,'mechanical');
#35157=PRODUCT('Pan Head Screw M3x25 1','Pan Head Screw M3x25 1',
'LEGAL AND USAGE DISCLAIMER: this Data/Model is provided \X2\201C\X0\A
S IS\X2\201D\X0\ for informational and representational only. It is a 
geometric approximation and is NOT engineered, certified, or guarantee
d for dimensional accuracy, exact tolerances, or production-level prec
ision. Vendor disclaims all implied warranties including fitness for a
 particular purpose. DO NOT USE FOR DIRECT PHYSICAL MANUFACTURING, AUT
OMATED PRODUCTION, OR SAFETY-CRITICAL SYSTEMS without independent engi
neering verification and resolution of any design discrepancies.',(#35123));
#35164=PRESENTATION_STYLE_ASSIGNMENT((#35173));
#35173=SURFACE_STYLE_USAGE(.BOTH.,#35182);
#35182=SURFACE_SIDE_STYLE('',(#35191));
#35191=SURFACE_STYLE_FILL_AREA(#35200);
#35200=FILL_AREA_STYLE('Plastic - Matte (White)',(#35209));
#35209=FILL_AREA_STYLE_COLOUR('Plastic - Matte (White)',#35218);
#35218=COLOUR_RGB('Plastic - Matte (White)',0.964705882352941,0.964705882352941,
0.952941176470588);
ENDSEC;
END-ISO-10303-21;
